ISO-10303-21;
HEADER;
/* Generated by software containing ST-Developer
 * from STEP Tools, Inc. (www.steptools.com) 
 */

FILE_DESCRIPTION(
/* description */ (''),
/* implementation_level */ '2;1');

FILE_NAME(
/* name */ '6661K61_Steel Ball Bearing.step',
/* time_stamp */ '2026-10-19T01:17:59+06:00',
/* author */ (''),
/* organization */ (''),
/* preprocessor_version */ 'ST-DEVELOPER v20.2',
/* originating_system */ 'Autodesk Translation Framework v15.15.0.0',
/* authorisation */ '');

FILE_SCHEMA (('AUTOMOTIVE_DESIGN { 1 0 10303 214 3 1 1 }'));
ENDSEC;

DATA;
#10=MECHANICAL_DESIGN_GEOMETRIC_PRESENTATION_REPRESENTATION('',(#735,#736,#737,#738,#739,#740,#741,#742,#743,#744,#745,#746),#48369);
#528=SPHERICAL_SURFACE('',#20866,3.828125);
#529=SPHERICAL_SURFACE('',#20923,3.828125);
#530=SPHERICAL_SURFACE('',#20925,3.828125);
#531=SPHERICAL_SURFACE('',#20927,3.828125);
#532=SPHERICAL_SURFACE('',#20929,3.828125);
#533=SPHERICAL_SURFACE('',#20931,3.828125);
#534=SPHERICAL_SURFACE('',#20933,3.828125);
#535=SPHERICAL_SURFACE('',#20935,3.828125);
#536=CONICAL_SURFACE('',#20738,13.867180376262,0.891067654753264);
#537=CONICAL_SURFACE('',#20759,12.7315647249454,0.891067654753261);
#538=CONICAL_SURFACE('',#20800,14.7602281873362,1.22173047639603);
#539=CONICAL_SURFACE('',#20802,14.7602281873362,1.22173047639603);
#540=CONICAL_SURFACE('',#20804,14.7602281873362,1.22173047639603);
#541=CONICAL_SURFACE('',#20806,14.7602281873362,1.22173047639603);
#542=CONICAL_SURFACE('',#20808,14.7602281873362,1.22173047639603);
#543=CONICAL_SURFACE('',#20810,14.7602281873362,1.22173047639603);
#544=CONICAL_SURFACE('',#20812,14.7602281873362,1.22173047639603);
#545=CONICAL_SURFACE('',#20814,14.7602281873362,1.22173047639603);
#546=CONICAL_SURFACE('',#20816,14.5602281873362,0.349065850398871);
#547=CONICAL_SURFACE('',#20818,14.5602281873362,0.349065850398871);
#548=CONICAL_SURFACE('',#20820,14.5602281873362,0.349065850398871);
#549=CONICAL_SURFACE('',#20822,14.5602281873362,0.349065850398871);
#550=CONICAL_SURFACE('',#20824,14.5602281873362,0.349065850398871);
#551=CONICAL_SURFACE('',#20826,14.5602281873362,0.349065850398871);
#552=CONICAL_SURFACE('',#20828,14.5602281873362,0.349065850398871);
#553=CONICAL_SURFACE('',#20830,14.5602281873362,0.349065850398871);
#554=CONICAL_SURFACE('',#20832,14.4779295903485,0.610865238198015);
#555=CONICAL_SURFACE('',#20833,14.4779295903485,0.610865238198015);
#556=CONICAL_SURFACE('',#20834,14.4779295903485,0.610865238198015);
#557=CONICAL_SURFACE('',#20835,14.4779295903485,0.610865238198015);
#558=CONICAL_SURFACE('',#20836,14.4779295903485,0.610865238198015);
#559=CONICAL_SURFACE('',#20837,14.4779295903485,0.610865238198015);
#560=CONICAL_SURFACE('',#20838,14.4779295903485,0.610865238198015);
#561=CONICAL_SURFACE('',#20839,14.4779295903485,0.610865238198015);
#562=CONICAL_SURFACE('',#20877,5.,0.122173047639596);
#563=CONICAL_SURFACE('',#20882,5.10805041359455,0.122173047639596);
#564=CONICAL_SURFACE('',#20909,16.796875,1.44862327915528);
#565=CONICAL_SURFACE('',#20911,17.0170281388728,1.44862327915529);
#566=CONICAL_SURFACE('',#20953,13.867180376262,0.891067654753264);
#567=CONICAL_SURFACE('',#20978,12.7315647249454,0.891067654753261);
#568=CONICAL_SURFACE('',#21014,14.7602281873362,1.22173047639603);
#569=CONICAL_SURFACE('',#21016,14.7602281873362,1.22173047639603);
#570=CONICAL_SURFACE('',#21018,14.7602281873362,1.22173047639603);
#571=CONICAL_SURFACE('',#21020,14.7602281873362,1.22173047639603);
#572=CONICAL_SURFACE('',#21022,14.7602281873362,1.22173047639603);
#573=CONICAL_SURFACE('',#21024,14.7602281873362,1.22173047639603);
#574=CONICAL_SURFACE('',#21026,14.7602281873362,1.22173047639603);
#575=CONICAL_SURFACE('',#21028,14.7602281873362,1.22173047639603);
#576=CONICAL_SURFACE('',#21030,14.5602281873362,0.349065850398871);
#577=CONICAL_SURFACE('',#21032,14.5602281873362,0.349065850398871);
#578=CONICAL_SURFACE('',#21034,14.5602281873362,0.349065850398871);
#579=CONICAL_SURFACE('',#21036,14.5602281873362,0.349065850398871);
#580=CONICAL_SURFACE('',#21038,14.5602281873362,0.349065850398871);
#581=CONICAL_SURFACE('',#21040,14.5602281873362,0.349065850398871);
#582=CONICAL_SURFACE('',#21042,14.5602281873362,0.349065850398871);
#583=CONICAL_SURFACE('',#21044,14.5602281873362,0.349065850398871);
#584=CONICAL_SURFACE('',#21046,14.4779295903485,0.610865238198015);
#585=CONICAL_SURFACE('',#21047,14.4779295903485,0.610865238198015);
#586=CONICAL_SURFACE('',#21048,14.4779295903485,0.610865238198015);
#587=CONICAL_SURFACE('',#21049,14.4779295903485,0.610865238198015);
#588=CONICAL_SURFACE('',#21050,14.4779295903485,0.610865238198015);
#589=CONICAL_SURFACE('',#21051,14.4779295903485,0.610865238198015);
#590=CONICAL_SURFACE('',#21052,14.4779295903485,0.610865238198015);
#591=CONICAL_SURFACE('',#21053,14.4779295903485,0.610865238198015);
#594=TOROIDAL_SURFACE('',#20731,8.781875,0.110000000000001);
#595=TOROIDAL_SURFACE('',#20734,9.6875,5.39274861573998);
#596=TOROIDAL_SURFACE('',#20740,14.3237119736335,0.726288026366507);
#597=TOROIDAL_SURFACE('',#20762,9.6875,4.84274861573998);
#598=TOROIDAL_SURFACE('',#20765,14.3237119736335,1.27628802636651);
#599=TOROIDAL_SURFACE('',#20868,12.03125,3.828125);
#600=TOROIDAL_SURFACE('',#20872,5.65395079699728,0.550000000000001);
#601=TOROIDAL_SURFACE('',#20884,5.65395079699728,0.550000000000001);
#602=TOROIDAL_SURFACE('',#20887,7.8875,0.55);
#603=TOROIDAL_SURFACE('',#20891,7.8875,0.55);
#604=TOROIDAL_SURFACE('',#20899,12.03125,3.828125);
#605=TOROIDAL_SURFACE('',#20906,16.95,0.55);
#606=TOROIDAL_SURFACE('',#20915,16.95,0.55);
#607=TOROIDAL_SURFACE('',#20937,12.03125,3.828125);
#608=TOROIDAL_SURFACE('',#20946,8.781875,0.110000000000001);
#609=TOROIDAL_SURFACE('',#20949,9.6875,5.39274861573998);
#610=TOROIDAL_SURFACE('',#20955,14.3237119736335,0.726288026366507);
#611=TOROIDAL_SURFACE('',#20974,9.6875,4.84274861573998);
#612=TOROIDAL_SURFACE('',#20979,14.3237119736335,1.27628802636651);
#615=SHAPE_REPRESENTATION_RELATIONSHIP('SRR','None',#48415,#626);
#626=ADVANCED_BREP_SHAPE_REPRESENTATION('',(#761,#762,#763,#764,#765,#766,
#767,#768,#769,#770,#771,#772),#48360);
#651=FACE_BOUND('',#2552,.T.);
#652=FACE_BOUND('',#2554,.T.);
#653=FACE_BOUND('',#2591,.T.);
#654=FACE_BOUND('',#2593,.T.);
#655=FACE_BOUND('',#2603,.T.);
#656=FACE_BOUND('',#2605,.T.);
#657=FACE_BOUND('',#2647,.T.);
#658=FACE_BOUND('',#2649,.T.);
#735=STYLED_ITEM('',(#48517),#761);
#736=STYLED_ITEM('',(#48517),#762);
#737=STYLED_ITEM('',(#48517),#763);
#738=STYLED_ITEM('',(#48517),#764);
#739=STYLED_ITEM('',(#48517),#765);
#740=STYLED_ITEM('',(#48517),#766);
#741=STYLED_ITEM('',(#48517),#767);
#742=STYLED_ITEM('',(#48517),#768);
#743=STYLED_ITEM('',(#48517),#769);
#744=STYLED_ITEM('',(#48517),#770);
#745=STYLED_ITEM('',(#48517),#771);
#746=STYLED_ITEM('',(#48517),#772);
#761=MANIFOLD_SOLID_BREP('Body1',#20114);
#762=MANIFOLD_SOLID_BREP('Body2',#20115);
#763=MANIFOLD_SOLID_BREP('Body3',#20116);
#764=MANIFOLD_SOLID_BREP('Body4',#20117);
#765=MANIFOLD_SOLID_BREP('Body5',#20118);
#766=MANIFOLD_SOLID_BREP('Body6',#20119);
#767=MANIFOLD_SOLID_BREP('Body7',#20120);
#768=MANIFOLD_SOLID_BREP('Body8',#20121);
#769=MANIFOLD_SOLID_BREP('Body9',#20122);
#770=MANIFOLD_SOLID_BREP('Body10',#20123);
#771=MANIFOLD_SOLID_BREP('Body11',#20124);
#772=MANIFOLD_SOLID_BREP('Body12',#20125);
#889=CYLINDRICAL_SURFACE('',#20728,8.671875);
#890=CYLINDRICAL_SURFACE('',#20880,5.);
#891=CYLINDRICAL_SURFACE('',#20895,8.4375);
#892=CYLINDRICAL_SURFACE('',#20896,8.4375);
#893=CYLINDRICAL_SURFACE('',#20903,17.5);
#894=CYLINDRICAL_SURFACE('',#20917,15.625);
#895=CYLINDRICAL_SURFACE('',#20919,15.625);
#896=CYLINDRICAL_SURFACE('',#20943,8.671875);
#1459=FACE_OUTER_BOUND('',#2519,.T.);
#1460=FACE_OUTER_BOUND('',#2520,.T.);
#1461=FACE_OUTER_BOUND('',#2521,.T.);
#1462=FACE_OUTER_BOUND('',#2522,.T.);
#1463=FACE_OUTER_BOUND('',#2523,.T.);
#1464=FACE_OUTER_BOUND('',#2524,.T.);
#1465=FACE_OUTER_BOUND('',#2525,.T.);
#1466=FACE_OUTER_BOUND('',#2526,.T.);
#1467=FACE_OUTER_BOUND('',#2527,.T.);
#1468=FACE_OUTER_BOUND('',#2528,.T.);
#1469=FACE_OUTER_BOUND('',#2529,.T.);
#1470=FACE_OUTER_BOUND('',#2530,.T.);
#1471=FACE_OUTER_BOUND('',#2531,.T.);
#1472=FACE_OUTER_BOUND('',#2532,.T.);
#1473=FACE_OUTER_BOUND('',#2533,.T.);
#1474=FACE_OUTER_BOUND('',#2534,.T.);
#1475=FACE_OUTER_BOUND('',#2535,.T.);
#1476=FACE_OUTER_BOUND('',#2536,.T.);
#1477=FACE_OUTER_BOUND('',#2537,.T.);
#1478=FACE_OUTER_BOUND('',#2538,.T.);
#1479=FACE_OUTER_BOUND('',#2539,.T.);
#1480=FACE_OUTER_BOUND('',#2540,.T.);
#1481=FACE_OUTER_BOUND('',#2541,.T.);
#1482=FACE_OUTER_BOUND('',#2542,.T.);
#1483=FACE_OUTER_BOUND('',#2543,.T.);
#1484=FACE_OUTER_BOUND('',#2544,.T.);
#1485=FACE_OUTER_BOUND('',#2545,.T.);
#1486=FACE_OUTER_BOUND('',#2546,.T.);
#1487=FACE_OUTER_BOUND('',#2547,.T.);
#1488=FACE_OUTER_BOUND('',#2548,.T.);
#1489=FACE_OUTER_BOUND('',#2549,.T.);
#1490=FACE_OUTER_BOUND('',#2550,.T.);
#1491=FACE_OUTER_BOUND('',#2551,.T.);
#1492=FACE_OUTER_BOUND('',#2553,.T.);
#1493=FACE_OUTER_BOUND('',#2555,.T.);
#1494=FACE_OUTER_BOUND('',#2556,.T.);
#1495=FACE_OUTER_BOUND('',#2557,.T.);
#1496=FACE_OUTER_BOUND('',#2558,.T.);
#1497=FACE_OUTER_BOUND('',#2559,.T.);
#1498=FACE_OUTER_BOUND('',#2560,.T.);
#1499=FACE_OUTER_BOUND('',#2561,.T.);
#1500=FACE_OUTER_BOUND('',#2562,.T.);
#1501=FACE_OUTER_BOUND('',#2563,.T.);
#1502=FACE_OUTER_BOUND('',#2564,.T.);
#1503=FACE_OUTER_BOUND('',#2565,.T.);
#1504=FACE_OUTER_BOUND('',#2566,.T.);
#1505=FACE_OUTER_BOUND('',#2567,.T.);
#1506=FACE_OUTER_BOUND('',#2568,.T.);
#1507=FACE_OUTER_BOUND('',#2569,.T.);
#1508=FACE_OUTER_BOUND('',#2570,.T.);
#1509=FACE_OUTER_BOUND('',#2571,.T.);
#1510=FACE_OUTER_BOUND('',#2572,.T.);
#1511=FACE_OUTER_BOUND('',#2573,.T.);
#1512=FACE_OUTER_BOUND('',#2574,.T.);
#1513=FACE_OUTER_BOUND('',#2575,.T.);
#1514=FACE_OUTER_BOUND('',#2576,.T.);
#1515=FACE_OUTER_BOUND('',#2577,.T.);
#1516=FACE_OUTER_BOUND('',#2578,.T.);
#1517=FACE_OUTER_BOUND('',#2579,.T.);
#1518=FACE_OUTER_BOUND('',#2580,.T.);
#1519=FACE_OUTER_BOUND('',#2581,.T.);
#1520=FACE_OUTER_BOUND('',#2582,.T.);
#1521=FACE_OUTER_BOUND('',#2583,.T.);
#1522=FACE_OUTER_BOUND('',#2584,.T.);
#1523=FACE_OUTER_BOUND('',#2585,.T.);
#1524=FACE_OUTER_BOUND('',#2586,.T.);
#1525=FACE_OUTER_BOUND('',#2587,.T.);
#1526=FACE_OUTER_BOUND('',#2588,.T.);
#1527=FACE_OUTER_BOUND('',#2589,.T.);
#1528=FACE_OUTER_BOUND('',#2590,.T.);
#1529=FACE_OUTER_BOUND('',#2592,.T.);
#1530=FACE_OUTER_BOUND('',#2594,.T.);
#1531=FACE_OUTER_BOUND('',#2595,.T.);
#1532=FACE_OUTER_BOUND('',#2596,.T.);
#1533=FACE_OUTER_BOUND('',#2597,.T.);
#1534=FACE_OUTER_BOUND('',#2598,.T.);
#1535=FACE_OUTER_BOUND('',#2599,.T.);
#1536=FACE_OUTER_BOUND('',#2600,.T.);
#1537=FACE_OUTER_BOUND('',#2601,.T.);
#1538=FACE_OUTER_BOUND('',#2602,.T.);
#1539=FACE_OUTER_BOUND('',#2604,.T.);
#1540=FACE_OUTER_BOUND('',#2606,.T.);
#1541=FACE_OUTER_BOUND('',#2607,.T.);
#1542=FACE_OUTER_BOUND('',#2608,.T.);
#1543=FACE_OUTER_BOUND('',#2609,.T.);
#1544=FACE_OUTER_BOUND('',#2610,.T.);
#1545=FACE_OUTER_BOUND('',#2611,.T.);
#1546=FACE_OUTER_BOUND('',#2612,.T.);
#1547=FACE_OUTER_BOUND('',#2613,.T.);
#1548=FACE_OUTER_BOUND('',#2614,.T.);
#1549=FACE_OUTER_BOUND('',#2615,.T.);
#1550=FACE_OUTER_BOUND('',#2616,.T.);
#1551=FACE_OUTER_BOUND('',#2617,.T.);
#1552=FACE_OUTER_BOUND('',#2618,.T.);
#1553=FACE_OUTER_BOUND('',#2619,.T.);
#1554=FACE_OUTER_BOUND('',#2620,.T.);
#1555=FACE_OUTER_BOUND('',#2621,.T.);
#1556=FACE_OUTER_BOUND('',#2622,.T.);
#1557=FACE_OUTER_BOUND('',#2623,.T.);
#1558=FACE_OUTER_BOUND('',#2624,.T.);
#1559=FACE_OUTER_BOUND('',#2625,.T.);
#1560=FACE_OUTER_BOUND('',#2626,.T.);
#1561=FACE_OUTER_BOUND('',#2627,.T.);
#1562=FACE_OUTER_BOUND('',#2628,.T.);
#1563=FACE_OUTER_BOUND('',#2629,.T.);
#1564=FACE_OUTER_BOUND('',#2630,.T.);
#1565=FACE_OUTER_BOUND('',#2631,.T.);
#1566=FACE_OUTER_BOUND('',#2632,.T.);
#1567=FACE_OUTER_BOUND('',#2633,.T.);
#1568=FACE_OUTER_BOUND('',#2634,.T.);
#1569=FACE_OUTER_BOUND('',#2635,.T.);
#1570=FACE_OUTER_BOUND('',#2636,.T.);
#1571=FACE_OUTER_BOUND('',#2637,.T.);
#1572=FACE_OUTER_BOUND('',#2638,.T.);
#1573=FACE_OUTER_BOUND('',#2639,.T.);
#1574=FACE_OUTER_BOUND('',#2640,.T.);
#1575=FACE_OUTER_BOUND('',#2641,.T.);
#1576=FACE_OUTER_BOUND('',#2642,.T.);
#1577=FACE_OUTER_BOUND('',#2643,.T.);
#1578=FACE_OUTER_BOUND('',#2644,.T.);
#1579=FACE_OUTER_BOUND('',#2645,.T.);
#1580=FACE_OUTER_BOUND('',#2646,.T.);
#1581=FACE_OUTER_BOUND('',#2648,.T.);
#1582=FACE_OUTER_BOUND('',#2650,.T.);
#1583=FACE_OUTER_BOUND('',#2651,.T.);
#1584=FACE_OUTER_BOUND('',#2652,.T.);
#1585=FACE_OUTER_BOUND('',#2653,.T.);
#1586=FACE_OUTER_BOUND('',#2654,.T.);
#1587=FACE_OUTER_BOUND('',#2655,.T.);
#1588=FACE_OUTER_BOUND('',#2656,.T.);
#1589=FACE_OUTER_BOUND('',#2657,.T.);
#1590=FACE_OUTER_BOUND('',#2658,.T.);
#1591=FACE_OUTER_BOUND('',#2659,.T.);
#1592=FACE_OUTER_BOUND('',#2660,.T.);
#1593=FACE_OUTER_BOUND('',#2661,.T.);
#1594=FACE_OUTER_BOUND('',#2662,.T.);
#1595=FACE_OUTER_BOUND('',#2663,.T.);
#1596=FACE_OUTER_BOUND('',#2664,.T.);
#1597=FACE_OUTER_BOUND('',#2665,.T.);
#1598=FACE_OUTER_BOUND('',#2666,.T.);
#1599=FACE_OUTER_BOUND('',#2667,.T.);
#1600=FACE_OUTER_BOUND('',#2668,.T.);
#1601=FACE_OUTER_BOUND('',#2669,.T.);
#1602=FACE_OUTER_BOUND('',#2670,.T.);
#1603=FACE_OUTER_BOUND('',#2671,.T.);
#1604=FACE_OUTER_BOUND('',#2672,.T.);
#1605=FACE_OUTER_BOUND('',#2673,.T.);
#2519=EDGE_LOOP('',(#14091,#14092,#14093,#14094));
#2520=EDGE_LOOP('',(#14095,#14096,#14097,#14098));
#2521=EDGE_LOOP('',(#14099,#14100,#14101,#14102));
#2522=EDGE_LOOP('',(#14103,#14104,#14105,#14106));
#2523=EDGE_LOOP('',(#14107,#14108,#14109,#14110,#14111,#14112,#14113,#14114,
#14115,#14116,#14117,#14118,#14119,#14120,#14121,#14122,#14123,#14124,#14125,
#14126));
#2524=EDGE_LOOP('',(#14127,#14128,#14129,#14130));
#2525=EDGE_LOOP('',(#14131,#14132,#14133,#14134));
#2526=EDGE_LOOP('',(#14135,#14136,#14137,#14138,#14139,#14140,#14141,#14142,
#14143,#14144,#14145,#14146,#14147,#14148,#14149,#14150,#14151,#14152,#14153,
#14154,#14155,#14156,#14157,#14158,#14159,#14160,#14161,#14162,#14163,#14164,
#14165,#14166,#14167,#14168,#14169,#14170));
#2527=EDGE_LOOP('',(#14171,#14172,#14173,#14174));
#2528=EDGE_LOOP('',(#14175,#14176,#14177,#14178));
#2529=EDGE_LOOP('',(#14179,#14180,#14181,#14182));
#2530=EDGE_LOOP('',(#14183,#14184,#14185,#14186));
#2531=EDGE_LOOP('',(#14187,#14188,#14189,#14190));
#2532=EDGE_LOOP('',(#14191,#14192,#14193,#14194));
#2533=EDGE_LOOP('',(#14195,#14196,#14197,#14198));
#2534=EDGE_LOOP('',(#14199,#14200,#14201,#14202));
#2535=EDGE_LOOP('',(#14203,#14204,#14205,#14206));
#2536=EDGE_LOOP('',(#14207,#14208,#14209,#14210));
#2537=EDGE_LOOP('',(#14211,#14212,#14213,#14214));
#2538=EDGE_LOOP('',(#14215,#14216,#14217,#14218));
#2539=EDGE_LOOP('',(#14219,#14220,#14221,#14222));
#2540=EDGE_LOOP('',(#14223,#14224,#14225,#14226));
#2541=EDGE_LOOP('',(#14227,#14228,#14229,#14230));
#2542=EDGE_LOOP('',(#14231,#14232,#14233,#14234));
#2543=EDGE_LOOP('',(#14235,#14236,#14237,#14238));
#2544=EDGE_LOOP('',(#14239,#14240,#14241,#14242));
#2545=EDGE_LOOP('',(#14243,#14244,#14245,#14246));
#2546=EDGE_LOOP('',(#14247,#14248,#14249,#14250));
#2547=EDGE_LOOP('',(#14251,#14252,#14253,#14254));
#2548=EDGE_LOOP('',(#14255,#14256,#14257,#14258));
#2549=EDGE_LOOP('',(#14259,#14260,#14261,#14262));
#2550=EDGE_LOOP('',(#14263,#14264,#14265,#14266));
#2551=EDGE_LOOP('',(#14267));
#2552=EDGE_LOOP('',(#14268));
#2553=EDGE_LOOP('',(#14269));
#2554=EDGE_LOOP('',(#14270));
#2555=EDGE_LOOP('',(#14271,#14272,#14273,#14274,#14275));
#2556=EDGE_LOOP('',(#14276,#14277,#14278,#14279,#14280));
#2557=EDGE_LOOP('',(#14281,#14282,#14283,#14284));
#2558=EDGE_LOOP('',(#14285,#14286,#14287,#14288,#14289));
#2559=EDGE_LOOP('',(#14290,#14291,#14292,#14293,#14294));
#2560=EDGE_LOOP('',(#14295,#14296,#14297,#14298));
#2561=EDGE_LOOP('',(#14299,#14300,#14301,#14302,#14303));
#2562=EDGE_LOOP('',(#14304,#14305,#14306,#14307,#14308));
#2563=EDGE_LOOP('',(#14309,#14310,#14311,#14312));
#2564=EDGE_LOOP('',(#14313,#14314,#14315,#14316,#14317));
#2565=EDGE_LOOP('',(#14318,#14319,#14320,#14321,#14322));
#2566=EDGE_LOOP('',(#14323,#14324,#14325,#14326));
#2567=EDGE_LOOP('',(#14327,#14328,#14329,#14330,#14331));
#2568=EDGE_LOOP('',(#14332,#14333,#14334,#14335,#14336));
#2569=EDGE_LOOP('',(#14337,#14338,#14339,#14340));
#2570=EDGE_LOOP('',(#14341,#14342,#14343,#14344,#14345));
#2571=EDGE_LOOP('',(#14346,#14347,#14348,#14349,#14350));
#2572=EDGE_LOOP('',(#14351,#14352,#14353,#14354));
#2573=EDGE_LOOP('',(#14355,#14356,#14357,#14358,#14359));
#2574=EDGE_LOOP('',(#14360,#14361,#14362,#14363,#14364));
#2575=EDGE_LOOP('',(#14365,#14366,#14367,#14368));
#2576=EDGE_LOOP('',(#14369,#14370,#14371,#14372,#14373));
#2577=EDGE_LOOP('',(#14374,#14375,#14376,#14377,#14378));
#2578=EDGE_LOOP('',(#14379,#14380,#14381,#14382,#14383,#14384));
#2579=EDGE_LOOP('',(#14385,#14386));
#2580=EDGE_LOOP('',(#14387,#14388,#14389,#14390));
#2581=EDGE_LOOP('',(#14391,#14392,#14393,#14394,#14395));
#2582=EDGE_LOOP('',(#14396,#14397,#14398,#14399,#14400,#14401));
#2583=EDGE_LOOP('',(#14402,#14403,#14404,#14405,#14406));
#2584=EDGE_LOOP('',(#14407,#14408,#14409,#14410));
#2585=EDGE_LOOP('',(#14411,#14412,#14413,#14414));
#2586=EDGE_LOOP('',(#14415,#14416,#14417,#14418));
#2587=EDGE_LOOP('',(#14419,#14420,#14421,#14422));
#2588=EDGE_LOOP('',(#14423,#14424,#14425,#14426));
#2589=EDGE_LOOP('',(#14427,#14428,#14429,#14430));
#2590=EDGE_LOOP('',(#14431));
#2591=EDGE_LOOP('',(#14432));
#2592=EDGE_LOOP('',(#14433));
#2593=EDGE_LOOP('',(#14434));
#2594=EDGE_LOOP('',(#14435,#14436,#14437,#14438));
#2595=EDGE_LOOP('',(#14439,#14440,#14441,#14442));
#2596=EDGE_LOOP('',(#14443,#14444,#14445,#14446));
#2597=EDGE_LOOP('',(#14447,#14448,#14449,#14450));
#2598=EDGE_LOOP('',(#14451,#14452,#14453,#14454,#14455));
#2599=EDGE_LOOP('',(#14456,#14457,#14458,#14459,#14460));
#2600=EDGE_LOOP('',(#14461,#14462,#14463,#14464));
#2601=EDGE_LOOP('',(#14465,#14466,#14467,#14468));
#2602=EDGE_LOOP('',(#14469));
#2603=EDGE_LOOP('',(#14470));
#2604=EDGE_LOOP('',(#14471));
#2605=EDGE_LOOP('',(#14472));
#2606=EDGE_LOOP('',(#14473,#14474));
#2607=EDGE_LOOP('',(#14475,#14476));
#2608=EDGE_LOOP('',(#14477,#14478));
#2609=EDGE_LOOP('',(#14479,#14480));
#2610=EDGE_LOOP('',(#14481,#14482));
#2611=EDGE_LOOP('',(#14483,#14484));
#2612=EDGE_LOOP('',(#14485,#14486));
#2613=EDGE_LOOP('',(#14487,#14488,#14489,#14490,#14491,#14492));
#2614=EDGE_LOOP('',(#14493,#14494,#14495,#14496));
#2615=EDGE_LOOP('',(#14497,#14498,#14499,#14500));
#2616=EDGE_LOOP('',(#14501,#14502,#14503,#14504));
#2617=EDGE_LOOP('',(#14505,#14506,#14507,#14508));
#2618=EDGE_LOOP('',(#14509,#14510,#14511,#14512,#14513,#14514,#14515,#14516,
#14517,#14518,#14519,#14520,#14521,#14522,#14523,#14524,#14525,#14526,#14527,
#14528));
#2619=EDGE_LOOP('',(#14529,#14530,#14531,#14532));
#2620=EDGE_LOOP('',(#14533,#14534,#14535,#14536,#14537));
#2621=EDGE_LOOP('',(#14538,#14539,#14540,#14541,#14542,#14543,#14544,#14545,
#14546,#14547,#14548,#14549,#14550,#14551,#14552,#14553,#14554,#14555,#14556,
#14557,#14558,#14559,#14560,#14561,#14562,#14563,#14564,#14565,#14566,#14567,
#14568,#14569,#14570,#14571,#14572,#14573,#14574));
#2622=EDGE_LOOP('',(#14575,#14576,#14577,#14578));
#2623=EDGE_LOOP('',(#14579,#14580,#14581,#14582));
#2624=EDGE_LOOP('',(#14583,#14584,#14585,#14586));
#2625=EDGE_LOOP('',(#14587,#14588,#14589,#14590));
#2626=EDGE_LOOP('',(#14591,#14592,#14593,#14594));
#2627=EDGE_LOOP('',(#14595,#14596,#14597,#14598));
#2628=EDGE_LOOP('',(#14599,#14600,#14601,#14602));
#2629=EDGE_LOOP('',(#14603,#14604,#14605,#14606));
#2630=EDGE_LOOP('',(#14607,#14608,#14609,#14610));
#2631=EDGE_LOOP('',(#14611,#14612,#14613,#14614));
#2632=EDGE_LOOP('',(#14615,#14616,#14617,#14618));
#2633=EDGE_LOOP('',(#14619,#14620,#14621,#14622));
#2634=EDGE_LOOP('',(#14623,#14624,#14625,#14626));
#2635=EDGE_LOOP('',(#14627,#14628,#14629,#14630));
#2636=EDGE_LOOP('',(#14631,#14632,#14633,#14634));
#2637=EDGE_LOOP('',(#14635,#14636,#14637,#14638));
#2638=EDGE_LOOP('',(#14639,#14640,#14641,#14642));
#2639=EDGE_LOOP('',(#14643,#14644,#14645,#14646));
#2640=EDGE_LOOP('',(#14647,#14648,#14649,#14650));
#2641=EDGE_LOOP('',(#14651,#14652,#14653,#14654));
#2642=EDGE_LOOP('',(#14655,#14656,#14657,#14658));
#2643=EDGE_LOOP('',(#14659,#14660,#14661,#14662));
#2644=EDGE_LOOP('',(#14663,#14664,#14665,#14666));
#2645=EDGE_LOOP('',(#14667,#14668,#14669,#14670));
#2646=EDGE_LOOP('',(#14671));
#2647=EDGE_LOOP('',(#14672));
#2648=EDGE_LOOP('',(#14673));
#2649=EDGE_LOOP('',(#14674));
#2650=EDGE_LOOP('',(#14675,#14676,#14677,#14678,#14679));
#2651=EDGE_LOOP('',(#14680,#14681,#14682,#14683,#14684));
#2652=EDGE_LOOP('',(#14685,#14686,#14687,#14688));
#2653=EDGE_LOOP('',(#14689,#14690,#14691,#14692,#14693));
#2654=EDGE_LOOP('',(#14694,#14695,#14696,#14697,#14698));
#2655=EDGE_LOOP('',(#14699,#14700,#14701,#14702));
#2656=EDGE_LOOP('',(#14703,#14704,#14705,#14706,#14707));
#2657=EDGE_LOOP('',(#14708,#14709,#14710,#14711,#14712));
#2658=EDGE_LOOP('',(#14713,#14714,#14715,#14716));
#2659=EDGE_LOOP('',(#14717,#14718,#14719,#14720,#14721));
#2660=EDGE_LOOP('',(#14722,#14723,#14724,#14725,#14726));
#2661=EDGE_LOOP('',(#14727,#14728,#14729,#14730));
#2662=EDGE_LOOP('',(#14731,#14732,#14733,#14734,#14735));
#2663=EDGE_LOOP('',(#14736,#14737,#14738,#14739,#14740));
#2664=EDGE_LOOP('',(#14741,#14742,#14743,#14744));
#2665=EDGE_LOOP('',(#14745,#14746,#14747,#14748,#14749));
#2666=EDGE_LOOP('',(#14750,#14751,#14752,#14753,#14754));
#2667=EDGE_LOOP('',(#14755,#14756,#14757,#14758));
#2668=EDGE_LOOP('',(#14759,#14760,#14761,#14762,#14763));
#2669=EDGE_LOOP('',(#14764,#14765,#14766,#14767,#14768));
#2670=EDGE_LOOP('',(#14769,#14770,#14771,#14772));
#2671=EDGE_LOOP('',(#14773,#14774,#14775,#14776,#14777));
#2672=EDGE_LOOP('',(#14778,#14779,#14780,#14781,#14782));
#2673=EDGE_LOOP('',(#14783,#14784,#14785,#14786,#14787,#14788));
#3605=CIRCLE('',#20729,8.671875);
#3606=CIRCLE('',#20730,8.671875);
#3607=CIRCLE('',#20732,8.781875);
#3608=CIRCLE('',#20733,0.110000000000001);
#3609=CIRCLE('',#20735,13.0772848379569);
#3610=CIRCLE('',#20736,5.39274861573998);
#3611=CIRCLE('',#20737,9.6875);
#3612=CIRCLE('',#20739,13.867180376262);
#3613=CIRCLE('',#20741,14.9186522951742);
#3614=CIRCLE('',#20742,14.9186522951742);
#3615=CIRCLE('',#20743,14.9186522951742);
#3616=CIRCLE('',#20744,14.9186522951742);
#3617=CIRCLE('',#20745,14.9186522951742);
#3618=CIRCLE('',#20746,14.9186522951742);
#3619=CIRCLE('',#20747,14.9186522951742);
#3620=CIRCLE('',#20748,14.9186522951742);
#3621=CIRCLE('',#20749,14.9186522951742);
#3622=CIRCLE('',#20750,0.726288026366507);
#3623=CIRCLE('',#20751,14.9186522951742);
#3624=CIRCLE('',#20752,14.9186522951742);
#3625=CIRCLE('',#20753,14.9186522951742);
#3626=CIRCLE('',#20754,14.9186522951742);
#3627=CIRCLE('',#20755,14.9186522951742);
#3628=CIRCLE('',#20756,14.9186522951742);
#3629=CIRCLE('',#20757,14.9186522951742);
#3630=CIRCLE('',#20758,14.9186522951742);
#3631=CIRCLE('',#20760,12.7315647249454);
#3632=CIRCLE('',#20761,13.5214602632505);
#3633=CIRCLE('',#20763,9.6875);
#3634=CIRCLE('',#20764,4.84274861573998);
#3635=CIRCLE('',#20766,1.27628802636651);
#3636=CIRCLE('',#20767,15.5300994798678);
#3637=CIRCLE('',#20768,1.27629997511691);
#3638=CIRCLE('',#20769,14.7602281873362);
#3639=CIRCLE('',#20770,1.27629996428189);
#3640=CIRCLE('',#20771,15.5300994798678);
#3641=CIRCLE('',#20772,1.27629997511692);
#3642=CIRCLE('',#20773,14.7602281873362);
#3643=CIRCLE('',#20774,1.27629996428189);
#3644=CIRCLE('',#20775,15.5300994798678);
#3645=CIRCLE('',#20776,1.27629997511692);
#3646=CIRCLE('',#20777,14.7602281873362);
#3647=CIRCLE('',#20778,1.27629996428189);
#3648=CIRCLE('',#20779,15.5300994798678);
#3649=CIRCLE('',#20780,1.27629997511691);
#3650=CIRCLE('',#20781,14.7602281873362);
#3651=CIRCLE('',#20782,1.27629996428186);
#3652=CIRCLE('',#20783,15.5300994798678);
#3653=CIRCLE('',#20784,1.27629997511693);
#3654=CIRCLE('',#20785,14.7602281873362);
#3655=CIRCLE('',#20786,1.27629996428187);
#3656=CIRCLE('',#20787,15.5300994798678);
#3657=CIRCLE('',#20788,1.27629997511691);
#3658=CIRCLE('',#20789,14.7602281873362);
#3659=CIRCLE('',#20790,1.27629996428189);
#3660=CIRCLE('',#20791,15.5300994798678);
#3661=CIRCLE('',#20792,1.27629997511692);
#3662=CIRCLE('',#20793,14.7602281873362);
#3663=CIRCLE('',#20794,1.27629996428189);
#3664=CIRCLE('',#20795,15.5300994798678);
#3665=CIRCLE('',#20796,1.27629997511693);
#3666=CIRCLE('',#20797,14.7602281873362);
#3667=CIRCLE('',#20798,1.27629996428189);
#3668=CIRCLE('',#20799,15.5300994798678);
#3669=CIRCLE('',#20801,14.5602281873362);
#3670=CIRCLE('',#20803,14.5602281873362);
#3671=CIRCLE('',#20805,14.5602281873362);
#3672=CIRCLE('',#20807,14.5602281873362);
#3673=CIRCLE('',#20809,14.5602281873362);
#3674=CIRCLE('',#20811,14.5602281873362);
#3675=CIRCLE('',#20813,14.5602281873362);
#3676=CIRCLE('',#20815,14.5602281873362);
#3677=CIRCLE('',#20817,14.4779295903485);
#3678=CIRCLE('',#20819,14.4779295903485);
#3679=CIRCLE('',#20821,14.4779295903485);
#3680=CIRCLE('',#20823,14.4779295903485);
#3681=CIRCLE('',#20825,14.4779295903485);
#3682=CIRCLE('',#20827,14.4779295903485);
#3683=CIRCLE('',#20829,14.4779295903485);
#3684=CIRCLE('',#20831,14.4779295903485);
#3685=CIRCLE('',#20867,3.828125);
#3686=CIRCLE('',#20869,8.4375);
#3687=CIRCLE('',#20870,3.828125);
#3688=CIRCLE('',#20871,8.4375);
#3689=CIRCLE('',#20873,5.44);
#3690=CIRCLE('',#20874,0.550000000000001);
#3691=CIRCLE('',#20875,5.10805041359455);
#3692=CIRCLE('',#20876,5.10805041359455);
#3693=CIRCLE('',#20878,5.);
#3694=CIRCLE('',#20879,5.);
#3695=CIRCLE('',#20881,5.);
#3696=CIRCLE('',#20883,5.10805041359455);
#3697=CIRCLE('',#20885,0.550000000000001);
#3698=CIRCLE('',#20886,5.44);
#3699=CIRCLE('',#20888,8.21796310590599);
#3700=CIRCLE('',#20889,0.55);
#3701=CIRCLE('',#20890,8.4375);
#3702=CIRCLE('',#20892,8.4375);
#3703=CIRCLE('',#20893,0.55);
#3704=CIRCLE('',#20894,8.21796310590599);
#3705=CIRCLE('',#20900,15.625);
#3706=CIRCLE('',#20901,3.828125);
#3707=CIRCLE('',#20902,15.625);
#3708=CIRCLE('',#20904,17.5);
#3709=CIRCLE('',#20905,17.5);
#3710=CIRCLE('',#20907,0.55);
#3711=CIRCLE('',#20908,17.0170281388728);
#3712=CIRCLE('',#20910,16.796875);
#3713=CIRCLE('',#20912,17.0170281388728);
#3714=CIRCLE('',#20913,16.796875);
#3715=CIRCLE('',#20914,17.0170281388728);
#3716=CIRCLE('',#20916,0.55);
#3717=CIRCLE('',#20918,15.625);
#3718=CIRCLE('',#20920,15.625);
#3719=CIRCLE('',#20924,3.828125);
#3720=CIRCLE('',#20926,3.828125);
#3721=CIRCLE('',#20928,3.828125);
#3722=CIRCLE('',#20930,3.828125);
#3723=CIRCLE('',#20932,3.828125);
#3724=CIRCLE('',#20934,3.828125);
#3725=CIRCLE('',#20936,3.828125);
#3726=CIRCLE('',#20938,14.46011695371);
#3727=CIRCLE('',#20939,14.46011695371);
#3728=CIRCLE('',#20940,3.828125);
#3729=CIRCLE('',#20941,12.9162151497931);
#3730=CIRCLE('',#20942,12.9162151497931);
#3731=CIRCLE('',#20944,8.671875);
#3732=CIRCLE('',#20945,8.671875);
#3733=CIRCLE('',#20947,8.781875);
#3734=CIRCLE('',#20948,0.110000000000001);
#3735=CIRCLE('',#20950,13.0772848379569);
#3736=CIRCLE('',#20951,5.39274861573998);
#3737=CIRCLE('',#20952,9.6875);
#3738=CIRCLE('',#20954,13.867180376262);
#3739=CIRCLE('',#20956,14.9186522951742);
#3740=CIRCLE('',#20957,14.9186522951742);
#3741=CIRCLE('',#20958,14.9186522951742);
#3742=CIRCLE('',#20959,14.9186522951742);
#3743=CIRCLE('',#20960,14.9186522951742);
#3744=CIRCLE('',#20961,14.9186522951742);
#3745=CIRCLE('',#20962,14.9186522951742);
#3746=CIRCLE('',#20963,14.9186522951742);
#3747=CIRCLE('',#20964,14.9186522951742);
#3748=CIRCLE('',#20965,0.726288026366507);
#3749=CIRCLE('',#20966,14.9186522951742);
#3750=CIRCLE('',#20967,14.9186522951742);
#3751=CIRCLE('',#20968,14.9186522951742);
#3752=CIRCLE('',#20969,14.9186522951742);
#3753=CIRCLE('',#20970,14.9186522951742);
#3754=CIRCLE('',#20971,14.9186522951742);
#3755=CIRCLE('',#20972,14.9186522951742);
#3756=CIRCLE('',#20973,14.9186522951742);
#3757=CIRCLE('',#20975,9.6875);
#3758=CIRCLE('',#20976,4.84274861573998);
#3759=CIRCLE('',#20977,12.7315647249454);
#3760=CIRCLE('',#20980,1.27628802636651);
#3761=CIRCLE('',#20981,15.5300994798678);
#3762=CIRCLE('',#20982,1.27629996428189);
#3763=CIRCLE('',#20983,14.7602281873362);
#3764=CIRCLE('',#20984,1.27629997511693);
#3765=CIRCLE('',#20985,15.5300994798678);
#3766=CIRCLE('',#20986,1.27629996428189);
#3767=CIRCLE('',#20987,14.7602281873362);
#3768=CIRCLE('',#20988,1.27629997511692);
#3769=CIRCLE('',#20989,15.5300994798678);
#3770=CIRCLE('',#20990,1.27629996428189);
#3771=CIRCLE('',#20991,14.7602281873362);
#3772=CIRCLE('',#20992,1.27629997511691);
#3773=CIRCLE('',#20993,15.5300994798678);
#3774=CIRCLE('',#20994,1.27629996428187);
#3775=CIRCLE('',#20995,14.7602281873362);
#3776=CIRCLE('',#20996,1.27629997511693);
#3777=CIRCLE('',#20997,15.5300994798678);
#3778=CIRCLE('',#20998,1.27629996428186);
#3779=CIRCLE('',#20999,14.7602281873362);
#3780=CIRCLE('',#21000,1.27629997511691);
#3781=CIRCLE('',#21001,15.5300994798678);
#3782=CIRCLE('',#21002,1.27629996428189);
#3783=CIRCLE('',#21003,14.7602281873362);
#3784=CIRCLE('',#21004,1.27629997511692);
#3785=CIRCLE('',#21005,15.5300994798678);
#3786=CIRCLE('',#21006,1.27629996428189);
#3787=CIRCLE('',#21007,14.7602281873362);
#3788=CIRCLE('',#21008,1.27629997511692);
#3789=CIRCLE('',#21009,15.5300994798678);
#3790=CIRCLE('',#21010,1.27629996428189);
#3791=CIRCLE('',#21011,14.7602281873362);
#3792=CIRCLE('',#21012,1.27629997511691);
#3793=CIRCLE('',#21013,15.5300994798678);
#3794=CIRCLE('',#21015,14.5602281873362);
#3795=CIRCLE('',#21017,14.5602281873362);
#3796=CIRCLE('',#21019,14.5602281873362);
#3797=CIRCLE('',#21021,14.5602281873362);
#3798=CIRCLE('',#21023,14.5602281873362);
#3799=CIRCLE('',#21025,14.5602281873362);
#3800=CIRCLE('',#21027,14.5602281873362);
#3801=CIRCLE('',#21029,14.5602281873362);
#3802=CIRCLE('',#21031,14.4779295903485);
#3803=CIRCLE('',#21033,14.4779295903485);
#3804=CIRCLE('',#21035,14.4779295903485);
#3805=CIRCLE('',#21037,14.4779295903485);
#3806=CIRCLE('',#21039,14.4779295903485);
#3807=CIRCLE('',#21041,14.4779295903485);
#3808=CIRCLE('',#21043,14.4779295903485);
#3809=CIRCLE('',#21045,14.4779295903485);
#4497=LINE('',#28607,#6378);
#4498=LINE('',#28622,#6379);
#4499=LINE('',#28663,#6380);
#4500=LINE('',#28739,#6381);
#4501=LINE('',#28742,#6382);
#4502=LINE('',#28747,#6383);
#4503=LINE('',#28748,#6384);
#4504=LINE('',#28751,#6385);
#4505=LINE('',#28754,#6386);
#4506=LINE('',#28757,#6387);
#4507=LINE('',#28760,#6388);
#4508=LINE('',#28763,#6389);
#4509=LINE('',#28766,#6390);
#4510=LINE('',#28769,#6391);
#4511=LINE('',#28772,#6392);
#4512=LINE('',#28775,#6393);
#4513=LINE('',#28778,#6394);
#4514=LINE('',#28783,#6395);
#4515=LINE('',#28784,#6396);
#4516=LINE('',#28787,#6397);
#4517=LINE('',#28790,#6398);
#4518=LINE('',#28795,#6399);
#4519=LINE('',#28796,#6400);
#4520=LINE('',#28799,#6401);
#4521=LINE('',#28802,#6402);
#4522=LINE('',#28805,#6403);
#4523=LINE('',#28808,#6404);
#4524=LINE('',#28811,#6405);
#4525=LINE('',#28814,#6406);
#4526=LINE('',#28817,#6407);
#4527=LINE('',#28820,#6408);
#4528=LINE('',#28823,#6409);
#4529=LINE('',#28826,#6410);
#4530=LINE('',#28831,#6411);
#4531=LINE('',#28832,#6412);
#4532=LINE('',#28834,#6413);
#4533=LINE('',#28835,#6414);
#4534=LINE('',#28837,#6415);
#4535=LINE('',#28838,#6416);
#4536=LINE('',#28840,#6417);
#4537=LINE('',#28841,#6418);
#4538=LINE('',#28843,#6419);
#4539=LINE('',#28844,#6420);
#4540=LINE('',#28846,#6421);
#4541=LINE('',#28847,#6422);
#4542=LINE('',#28849,#6423);
#4543=LINE('',#28850,#6424);
#4544=LINE('',#28852,#6425);
#4545=LINE('',#28853,#6426);
#4546=LINE('',#28855,#6427);
#4547=LINE('',#28856,#6428);
#4548=LINE('',#28860,#6429);
#4549=LINE('',#28862,#6430);
#4550=LINE('',#28865,#6431);
#4551=LINE('',#28867,#6432);
#4552=LINE('',#28870,#6433);
#4553=LINE('',#28872,#6434);
#4554=LINE('',#28875,#6435);
#4555=LINE('',#28877,#6436);
#4556=LINE('',#28880,#6437);
#4557=LINE('',#28882,#6438);
#4558=LINE('',#28885,#6439);
#4559=LINE('',#28887,#6440);
#4560=LINE('',#28890,#6441);
#4561=LINE('',#28892,#6442);
#4562=LINE('',#28895,#6443);
#4563=LINE('',#28897,#6444);
#4564=LINE('',#28921,#6445);
#4565=LINE('',#28925,#6446);
#4566=LINE('',#28929,#6447);
#4567=LINE('',#28948,#6448);
#4568=LINE('',#28950,#6449);
#4569=LINE('',#28963,#6450);
#4570=LINE('',#28971,#6451);
#4571=LINE('',#28978,#6452);
#4572=LINE('',#28986,#6453);
#4573=LINE('',#28989,#6454);
#4574=LINE('',#29035,#6455);
#4575=LINE('',#29050,#6456);
#4576=LINE('',#29094,#6457);
#4577=LINE('',#29165,#6458);
#4578=LINE('',#29168,#6459);
#4579=LINE('',#29173,#6460);
#4580=LINE('',#29174,#6461);
#4581=LINE('',#29177,#6462);
#4582=LINE('',#29180,#6463);
#4583=LINE('',#29183,#6464);
#4584=LINE('',#29186,#6465);
#4585=LINE('',#29189,#6466);
#4586=LINE('',#29192,#6467);
#4587=LINE('',#29195,#6468);
#4588=LINE('',#29198,#6469);
#4589=LINE('',#29201,#6470);
#4590=LINE('',#29204,#6471);
#4591=LINE('',#29209,#6472);
#4592=LINE('',#29210,#6473);
#4593=LINE('',#29213,#6474);
#4594=LINE('',#29216,#6475);
#4595=LINE('',#29221,#6476);
#4596=LINE('',#29222,#6477);
#4597=LINE('',#29225,#6478);
#4598=LINE('',#29228,#6479);
#4599=LINE('',#29231,#6480);
#4600=LINE('',#29234,#6481);
#4601=LINE('',#29237,#6482);
#4602=LINE('',#29240,#6483);
#4603=LINE('',#29243,#6484);
#4604=LINE('',#29246,#6485);
#4605=LINE('',#29249,#6486);
#4606=LINE('',#29252,#6487);
#4607=LINE('',#29257,#6488);
#4608=LINE('',#29258,#6489);
#4609=LINE('',#29260,#6490);
#4610=LINE('',#29261,#6491);
#4611=LINE('',#29263,#6492);
#4612=LINE('',#29264,#6493);
#4613=LINE('',#29266,#6494);
#4614=LINE('',#29267,#6495);
#4615=LINE('',#29269,#6496);
#4616=LINE('',#29270,#6497);
#4617=LINE('',#29272,#6498);
#4618=LINE('',#29273,#6499);
#4619=LINE('',#29275,#6500);
#4620=LINE('',#29276,#6501);
#4621=LINE('',#29278,#6502);
#4622=LINE('',#29279,#6503);
#4623=LINE('',#29281,#6504);
#4624=LINE('',#29282,#6505);
#4625=LINE('',#29286,#6506);
#4626=LINE('',#29288,#6507);
#4627=LINE('',#29291,#6508);
#4628=LINE('',#29293,#6509);
#4629=LINE('',#29296,#6510);
#4630=LINE('',#29298,#6511);
#4631=LINE('',#29301,#6512);
#4632=LINE('',#29303,#6513);
#4633=LINE('',#29306,#6514);
#4634=LINE('',#29308,#6515);
#4635=LINE('',#29311,#6516);
#4636=LINE('',#29313,#6517);
#4637=LINE('',#29316,#6518);
#4638=LINE('',#29318,#6519);
#4639=LINE('',#29321,#6520);
#4640=LINE('',#29323,#6521);
#6378=VECTOR('',#23378,8.671875);
#6379=VECTOR('',#23399,13.867180376262);
#6380=VECTOR('',#23442,12.7315647249454);
#6381=VECTOR('',#23523,10.);
#6382=VECTOR('',#23526,10.);
#6383=VECTOR('',#23531,10.);
#6384=VECTOR('',#23532,10.);
#6385=VECTOR('',#23535,10.);
#6386=VECTOR('',#23538,10.);
#6387=VECTOR('',#23541,10.);
#6388=VECTOR('',#23544,10.);
#6389=VECTOR('',#23547,10.);
#6390=VECTOR('',#23550,10.);
#6391=VECTOR('',#23553,10.);
#6392=VECTOR('',#23556,10.);
#6393=VECTOR('',#23559,10.);
#6394=VECTOR('',#23562,10.);
#6395=VECTOR('',#23567,10.);
#6396=VECTOR('',#23568,10.);
#6397=VECTOR('',#23571,10.);
#6398=VECTOR('',#23574,10.);
#6399=VECTOR('',#23579,10.);
#6400=VECTOR('',#23580,10.);
#6401=VECTOR('',#23583,10.);
#6402=VECTOR('',#23586,10.);
#6403=VECTOR('',#23589,10.);
#6404=VECTOR('',#23592,10.);
#6405=VECTOR('',#23595,10.);
#6406=VECTOR('',#23598,10.);
#6407=VECTOR('',#23601,10.);
#6408=VECTOR('',#23604,10.);
#6409=VECTOR('',#23607,10.);
#6410=VECTOR('',#23610,10.);
#6411=VECTOR('',#23615,10.);
#6412=VECTOR('',#23616,10.);
#6413=VECTOR('',#23619,10.);
#6414=VECTOR('',#23620,10.);
#6415=VECTOR('',#23623,10.);
#6416=VECTOR('',#23624,10.);
#6417=VECTOR('',#23627,10.);
#6418=VECTOR('',#23628,10.);
#6419=VECTOR('',#23631,10.);
#6420=VECTOR('',#23632,10.);
#6421=VECTOR('',#23635,10.);
#6422=VECTOR('',#23636,10.);
#6423=VECTOR('',#23639,10.);
#6424=VECTOR('',#23640,10.);
#6425=VECTOR('',#23643,10.);
#6426=VECTOR('',#23644,10.);
#6427=VECTOR('',#23647,10.);
#6428=VECTOR('',#23648,10.);
#6429=VECTOR('',#23655,1000.);
#6430=VECTOR('',#23658,1000.);
#6431=VECTOR('',#23663,1000.);
#6432=VECTOR('',#23666,1000.);
#6433=VECTOR('',#23671,1000.);
#6434=VECTOR('',#23674,1000.);
#6435=VECTOR('',#23679,1000.);
#6436=VECTOR('',#23682,1000.);
#6437=VECTOR('',#23687,1000.);
#6438=VECTOR('',#23690,1000.);
#6439=VECTOR('',#23695,1000.);
#6440=VECTOR('',#23698,1000.);
#6441=VECTOR('',#23703,1000.);
#6442=VECTOR('',#23706,1000.);
#6443=VECTOR('',#23711,1000.);
#6444=VECTOR('',#23714,1000.);
#6445=VECTOR('',#23743,5.);
#6446=VECTOR('',#23748,5.);
#6447=VECTOR('',#23753,5.10805041359455);
#6448=VECTOR('',#23780,8.4375);
#6449=VECTOR('',#23783,8.4375);
#6450=VECTOR('',#23800,17.5);
#6451=VECTOR('',#23811,16.796875);
#6452=VECTOR('',#23818,17.0170281388728);
#6453=VECTOR('',#23831,15.625);
#6454=VECTOR('',#23834,15.625);
#6455=VECTOR('',#23885,8.671875);
#6456=VECTOR('',#23906,13.867180376262);
#6457=VECTOR('',#23955,12.7315647249454);
#6458=VECTOR('',#24028,10.);
#6459=VECTOR('',#24031,10.);
#6460=VECTOR('',#24036,10.);
#6461=VECTOR('',#24037,10.);
#6462=VECTOR('',#24040,10.);
#6463=VECTOR('',#24043,10.);
#6464=VECTOR('',#24046,10.);
#6465=VECTOR('',#24049,10.);
#6466=VECTOR('',#24052,10.);
#6467=VECTOR('',#24055,10.);
#6468=VECTOR('',#24058,10.);
#6469=VECTOR('',#24061,10.);
#6470=VECTOR('',#24064,10.);
#6471=VECTOR('',#24067,10.);
#6472=VECTOR('',#24072,10.);
#6473=VECTOR('',#24073,10.);
#6474=VECTOR('',#24076,10.);
#6475=VECTOR('',#24079,10.);
#6476=VECTOR('',#24084,10.);
#6477=VECTOR('',#24085,10.);
#6478=VECTOR('',#24088,10.);
#6479=VECTOR('',#24091,10.);
#6480=VECTOR('',#24094,10.);
#6481=VECTOR('',#24097,10.);
#6482=VECTOR('',#24100,10.);
#6483=VECTOR('',#24103,10.);
#6484=VECTOR('',#24106,10.);
#6485=VECTOR('',#24109,10.);
#6486=VECTOR('',#24112,10.);
#6487=VECTOR('',#24115,10.);
#6488=VECTOR('',#24120,10.);
#6489=VECTOR('',#24121,10.);
#6490=VECTOR('',#24124,10.);
#6491=VECTOR('',#24125,10.);
#6492=VECTOR('',#24128,10.);
#6493=VECTOR('',#24129,10.);
#6494=VECTOR('',#24132,10.);
#6495=VECTOR('',#24133,10.);
#6496=VECTOR('',#24136,10.);
#6497=VECTOR('',#24137,10.);
#6498=VECTOR('',#24140,10.);
#6499=VECTOR('',#24141,10.);
#6500=VECTOR('',#24144,10.);
#6501=VECTOR('',#24145,10.);
#6502=VECTOR('',#24148,10.);
#6503=VECTOR('',#24149,10.);
#6504=VECTOR('',#24152,10.);
#6505=VECTOR('',#24153,10.);
#6506=VECTOR('',#24160,1000.);
#6507=VECTOR('',#24163,1000.);
#6508=VECTOR('',#24168,1000.);
#6509=VECTOR('',#24171,1000.);
#6510=VECTOR('',#24176,1000.);
#6511=VECTOR('',#24179,1000.);
#6512=VECTOR('',#24184,1000.);
#6513=VECTOR('',#24187,1000.);
#6514=VECTOR('',#24192,1000.);
#6515=VECTOR('',#24195,1000.);
#6516=VECTOR('',#24200,1000.);
#6517=VECTOR('',#24203,1000.);
#6518=VECTOR('',#24208,1000.);
#6519=VECTOR('',#24211,1000.);
#6520=VECTOR('',#24216,1000.);
#6521=VECTOR('',#24219,1000.);
#8235=VERTEX_POINT('',#28604);
#8236=VERTEX_POINT('',#28606);
#8237=VERTEX_POINT('',#28610);
#8238=VERTEX_POINT('',#28614);
#8239=VERTEX_POINT('',#28616);
#8240=VERTEX_POINT('',#28620);
#8241=VERTEX_POINT('',#28624);
#8242=VERTEX_POINT('',#28625);
#8243=VERTEX_POINT('',#28627);
#8244=VERTEX_POINT('',#28629);
#8245=VERTEX_POINT('',#28631);
#8246=VERTEX_POINT('',#28633);
#8247=VERTEX_POINT('',#28635);
#8248=VERTEX_POINT('',#28637);
#8249=VERTEX_POINT('',#28639);
#8250=VERTEX_POINT('',#28641);
#8251=VERTEX_POINT('',#28644);
#8252=VERTEX_POINT('',#28646);
#8253=VERTEX_POINT('',#28648);
#8254=VERTEX_POINT('',#28650);
#8255=VERTEX_POINT('',#28652);
#8256=VERTEX_POINT('',#28654);
#8257=VERTEX_POINT('',#28656);
#8258=VERTEX_POINT('',#28660);
#8259=VERTEX_POINT('',#28662);
#8260=VERTEX_POINT('',#28666);
#8261=VERTEX_POINT('',#28670);
#8262=VERTEX_POINT('',#28672);
#8263=VERTEX_POINT('',#28674);
#8264=VERTEX_POINT('',#28676);
#8265=VERTEX_POINT('',#28678);
#8266=VERTEX_POINT('',#28680);
#8267=VERTEX_POINT('',#28682);
#8268=VERTEX_POINT('',#28684);
#8269=VERTEX_POINT('',#28686);
#8270=VERTEX_POINT('',#28688);
#8271=VERTEX_POINT('',#28690);
#8272=VERTEX_POINT('',#28692);
#8273=VERTEX_POINT('',#28694);
#8274=VERTEX_POINT('',#28696);
#8275=VERTEX_POINT('',#28698);
#8276=VERTEX_POINT('',#28700);
#8277=VERTEX_POINT('',#28702);
#8278=VERTEX_POINT('',#28704);
#8279=VERTEX_POINT('',#28706);
#8280=VERTEX_POINT('',#28708);
#8281=VERTEX_POINT('',#28710);
#8282=VERTEX_POINT('',#28712);
#8283=VERTEX_POINT('',#28714);
#8284=VERTEX_POINT('',#28716);
#8285=VERTEX_POINT('',#28718);
#8286=VERTEX_POINT('',#28720);
#8287=VERTEX_POINT('',#28722);
#8288=VERTEX_POINT('',#28724);
#8289=VERTEX_POINT('',#28726);
#8290=VERTEX_POINT('',#28728);
#8291=VERTEX_POINT('',#28730);
#8292=VERTEX_POINT('',#28732);
#8293=VERTEX_POINT('',#28734);
#8294=VERTEX_POINT('',#28738);
#8295=VERTEX_POINT('',#28740);
#8296=VERTEX_POINT('',#28744);
#8297=VERTEX_POINT('',#28745);
#8298=VERTEX_POINT('',#28750);
#8299=VERTEX_POINT('',#28752);
#8300=VERTEX_POINT('',#28756);
#8301=VERTEX_POINT('',#28758);
#8302=VERTEX_POINT('',#28762);
#8303=VERTEX_POINT('',#28764);
#8304=VERTEX_POINT('',#28768);
#8305=VERTEX_POINT('',#28770);
#8306=VERTEX_POINT('',#28774);
#8307=VERTEX_POINT('',#28776);
#8308=VERTEX_POINT('',#28780);
#8309=VERTEX_POINT('',#28781);
#8310=VERTEX_POINT('',#28786);
#8311=VERTEX_POINT('',#28788);
#8312=VERTEX_POINT('',#28792);
#8313=VERTEX_POINT('',#28793);
#8314=VERTEX_POINT('',#28798);
#8315=VERTEX_POINT('',#28800);
#8316=VERTEX_POINT('',#28804);
#8317=VERTEX_POINT('',#28806);
#8318=VERTEX_POINT('',#28810);
#8319=VERTEX_POINT('',#28812);
#8320=VERTEX_POINT('',#28816);
#8321=VERTEX_POINT('',#28818);
#8322=VERTEX_POINT('',#28822);
#8323=VERTEX_POINT('',#28824);
#8324=VERTEX_POINT('',#28828);
#8325=VERTEX_POINT('',#28829);
#8326=VERTEX_POINT('',#28900);
#8327=VERTEX_POINT('',#28901);
#8328=VERTEX_POINT('',#28904);
#8329=VERTEX_POINT('',#28906);
#8330=VERTEX_POINT('',#28910);
#8331=VERTEX_POINT('',#28912);
#8332=VERTEX_POINT('',#28914);
#8333=VERTEX_POINT('',#28918);
#8334=VERTEX_POINT('',#28919);
#8335=VERTEX_POINT('',#28924);
#8336=VERTEX_POINT('',#28928);
#8337=VERTEX_POINT('',#28932);
#8338=VERTEX_POINT('',#28936);
#8339=VERTEX_POINT('',#28938);
#8340=VERTEX_POINT('',#28942);
#8341=VERTEX_POINT('',#28944);
#8342=VERTEX_POINT('',#28954);
#8343=VERTEX_POINT('',#28956);
#8344=VERTEX_POINT('',#28960);
#8345=VERTEX_POINT('',#28962);
#8346=VERTEX_POINT('',#28966);
#8347=VERTEX_POINT('',#28970);
#8348=VERTEX_POINT('',#28974);
#8349=VERTEX_POINT('',#28975);
#8350=VERTEX_POINT('',#28977);
#8351=VERTEX_POINT('',#28984);
#8352=VERTEX_POINT('',#28988);
#8353=VERTEX_POINT('',#28994);
#8354=VERTEX_POINT('',#28995);
#8355=VERTEX_POINT('',#28998);
#8356=VERTEX_POINT('',#28999);
#8357=VERTEX_POINT('',#29002);
#8358=VERTEX_POINT('',#29003);
#8359=VERTEX_POINT('',#29006);
#8360=VERTEX_POINT('',#29007);
#8361=VERTEX_POINT('',#29010);
#8362=VERTEX_POINT('',#29011);
#8363=VERTEX_POINT('',#29014);
#8364=VERTEX_POINT('',#29015);
#8365=VERTEX_POINT('',#29018);
#8366=VERTEX_POINT('',#29019);
#8367=VERTEX_POINT('',#29022);
#8368=VERTEX_POINT('',#29023);
#8369=VERTEX_POINT('',#29026);
#8370=VERTEX_POINT('',#29028);
#8371=VERTEX_POINT('',#29032);
#8372=VERTEX_POINT('',#29034);
#8373=VERTEX_POINT('',#29038);
#8374=VERTEX_POINT('',#29042);
#8375=VERTEX_POINT('',#29044);
#8376=VERTEX_POINT('',#29048);
#8377=VERTEX_POINT('',#29052);
#8378=VERTEX_POINT('',#29053);
#8379=VERTEX_POINT('',#29055);
#8380=VERTEX_POINT('',#29057);
#8381=VERTEX_POINT('',#29059);
#8382=VERTEX_POINT('',#29061);
#8383=VERTEX_POINT('',#29063);
#8384=VERTEX_POINT('',#29065);
#8385=VERTEX_POINT('',#29067);
#8386=VERTEX_POINT('',#29069);
#8387=VERTEX_POINT('',#29072);
#8388=VERTEX_POINT('',#29074);
#8389=VERTEX_POINT('',#29076);
#8390=VERTEX_POINT('',#29078);
#8391=VERTEX_POINT('',#29080);
#8392=VERTEX_POINT('',#29082);
#8393=VERTEX_POINT('',#29084);
#8394=VERTEX_POINT('',#29088);
#8395=VERTEX_POINT('',#29090);
#8396=VERTEX_POINT('',#29096);
#8397=VERTEX_POINT('',#29098);
#8398=VERTEX_POINT('',#29100);
#8399=VERTEX_POINT('',#29102);
#8400=VERTEX_POINT('',#29104);
#8401=VERTEX_POINT('',#29106);
#8402=VERTEX_POINT('',#29108);
#8403=VERTEX_POINT('',#29110);
#8404=VERTEX_POINT('',#29112);
#8405=VERTEX_POINT('',#29114);
#8406=VERTEX_POINT('',#29116);
#8407=VERTEX_POINT('',#29118);
#8408=VERTEX_POINT('',#29120);
#8409=VERTEX_POINT('',#29122);
#8410=VERTEX_POINT('',#29124);
#8411=VERTEX_POINT('',#29126);
#8412=VERTEX_POINT('',#29128);
#8413=VERTEX_POINT('',#29130);
#8414=VERTEX_POINT('',#29132);
#8415=VERTEX_POINT('',#29134);
#8416=VERTEX_POINT('',#29136);
#8417=VERTEX_POINT('',#29138);
#8418=VERTEX_POINT('',#29140);
#8419=VERTEX_POINT('',#29142);
#8420=VERTEX_POINT('',#29144);
#8421=VERTEX_POINT('',#29146);
#8422=VERTEX_POINT('',#29148);
#8423=VERTEX_POINT('',#29150);
#8424=VERTEX_POINT('',#29152);
#8425=VERTEX_POINT('',#29154);
#8426=VERTEX_POINT('',#29156);
#8427=VERTEX_POINT('',#29158);
#8428=VERTEX_POINT('',#29160);
#8429=VERTEX_POINT('',#29164);
#8430=VERTEX_POINT('',#29166);
#8431=VERTEX_POINT('',#29170);
#8432=VERTEX_POINT('',#29171);
#8433=VERTEX_POINT('',#29176);
#8434=VERTEX_POINT('',#29178);
#8435=VERTEX_POINT('',#29182);
#8436=VERTEX_POINT('',#29184);
#8437=VERTEX_POINT('',#29188);
#8438=VERTEX_POINT('',#29190);
#8439=VERTEX_POINT('',#29194);
#8440=VERTEX_POINT('',#29196);
#8441=VERTEX_POINT('',#29200);
#8442=VERTEX_POINT('',#29202);
#8443=VERTEX_POINT('',#29206);
#8444=VERTEX_POINT('',#29207);
#8445=VERTEX_POINT('',#29212);
#8446=VERTEX_POINT('',#29214);
#8447=VERTEX_POINT('',#29218);
#8448=VERTEX_POINT('',#29219);
#8449=VERTEX_POINT('',#29224);
#8450=VERTEX_POINT('',#29226);
#8451=VERTEX_POINT('',#29230);
#8452=VERTEX_POINT('',#29232);
#8453=VERTEX_POINT('',#29236);
#8454=VERTEX_POINT('',#29238);
#8455=VERTEX_POINT('',#29242);
#8456=VERTEX_POINT('',#29244);
#8457=VERTEX_POINT('',#29248);
#8458=VERTEX_POINT('',#29250);
#8459=VERTEX_POINT('',#29254);
#8460=VERTEX_POINT('',#29255);
#10429=EDGE_CURVE('',#8235,#8235,#3605,.T.);
#10430=EDGE_CURVE('',#8235,#8236,#4497,.T.);
#10431=EDGE_CURVE('',#8236,#8236,#3606,.T.);
#10432=EDGE_CURVE('',#8237,#8237,#3607,.T.);
#10433=EDGE_CURVE('',#8237,#8235,#3608,.T.);
#10434=EDGE_CURVE('',#8238,#8238,#3609,.T.);
#10435=EDGE_CURVE('',#8238,#8239,#3610,.T.);
#10436=EDGE_CURVE('',#8239,#8239,#3611,.T.);
#10437=EDGE_CURVE('',#8240,#8240,#3612,.T.);
#10438=EDGE_CURVE('',#8240,#8238,#4498,.T.);
#10439=EDGE_CURVE('',#8241,#8242,#3613,.T.);
#10440=EDGE_CURVE('',#8242,#8243,#3614,.T.);
#10441=EDGE_CURVE('',#8243,#8244,#3615,.T.);
#10442=EDGE_CURVE('',#8244,#8245,#3616,.T.);
#10443=EDGE_CURVE('',#8245,#8246,#3617,.T.);
#10444=EDGE_CURVE('',#8246,#8247,#3618,.T.);
#10445=EDGE_CURVE('',#8247,#8248,#3619,.T.);
#10446=EDGE_CURVE('',#8248,#8249,#3620,.T.);
#10447=EDGE_CURVE('',#8249,#8250,#3621,.T.);
#10448=EDGE_CURVE('',#8250,#8240,#3622,.T.);
#10449=EDGE_CURVE('',#8250,#8251,#3623,.T.);
#10450=EDGE_CURVE('',#8251,#8252,#3624,.T.);
#10451=EDGE_CURVE('',#8252,#8253,#3625,.T.);
#10452=EDGE_CURVE('',#8253,#8254,#3626,.T.);
#10453=EDGE_CURVE('',#8254,#8255,#3627,.T.);
#10454=EDGE_CURVE('',#8255,#8256,#3628,.T.);
#10455=EDGE_CURVE('',#8256,#8257,#3629,.T.);
#10456=EDGE_CURVE('',#8257,#8241,#3630,.T.);
#10457=EDGE_CURVE('',#8258,#8258,#3631,.T.);
#10458=EDGE_CURVE('',#8258,#8259,#4499,.T.);
#10459=EDGE_CURVE('',#8259,#8259,#3632,.T.);
#10460=EDGE_CURVE('',#8260,#8260,#3633,.T.);
#10461=EDGE_CURVE('',#8260,#8258,#3634,.T.);
#10462=EDGE_CURVE('',#8259,#8261,#3635,.T.);
#10463=EDGE_CURVE('',#8261,#8262,#3636,.T.);
#10464=EDGE_CURVE('',#8263,#8262,#3637,.T.);
#10465=EDGE_CURVE('',#8264,#8263,#3638,.T.);
#10466=EDGE_CURVE('',#8265,#8264,#3639,.T.);
#10467=EDGE_CURVE('',#8265,#8266,#3640,.T.);
#10468=EDGE_CURVE('',#8267,#8266,#3641,.T.);
#10469=EDGE_CURVE('',#8268,#8267,#3642,.T.);
#10470=EDGE_CURVE('',#8269,#8268,#3643,.T.);
#10471=EDGE_CURVE('',#8269,#8270,#3644,.T.);
#10472=EDGE_CURVE('',#8271,#8270,#3645,.T.);
#10473=EDGE_CURVE('',#8272,#8271,#3646,.T.);
#10474=EDGE_CURVE('',#8273,#8272,#3647,.T.);
#10475=EDGE_CURVE('',#8273,#8274,#3648,.T.);
#10476=EDGE_CURVE('',#8275,#8274,#3649,.T.);
#10477=EDGE_CURVE('',#8276,#8275,#3650,.T.);
#10478=EDGE_CURVE('',#8277,#8276,#3651,.T.);
#10479=EDGE_CURVE('',#8277,#8278,#3652,.T.);
#10480=EDGE_CURVE('',#8279,#8278,#3653,.T.);
#10481=EDGE_CURVE('',#8280,#8279,#3654,.T.);
#10482=EDGE_CURVE('',#8281,#8280,#3655,.T.);
#10483=EDGE_CURVE('',#8281,#8282,#3656,.T.);
#10484=EDGE_CURVE('',#8283,#8282,#3657,.T.);
#10485=EDGE_CURVE('',#8284,#8283,#3658,.T.);
#10486=EDGE_CURVE('',#8285,#8284,#3659,.T.);
#10487=EDGE_CURVE('',#8285,#8286,#3660,.T.);
#10488=EDGE_CURVE('',#8287,#8286,#3661,.T.);
#10489=EDGE_CURVE('',#8288,#8287,#3662,.T.);
#10490=EDGE_CURVE('',#8289,#8288,#3663,.T.);
#10491=EDGE_CURVE('',#8289,#8290,#3664,.T.);
#10492=EDGE_CURVE('',#8291,#8290,#3665,.T.);
#10493=EDGE_CURVE('',#8292,#8291,#3666,.T.);
#10494=EDGE_CURVE('',#8293,#8292,#3667,.T.);
#10495=EDGE_CURVE('',#8293,#8261,#3668,.T.);
#10496=EDGE_CURVE('',#8294,#8291,#4500,.T.);
#10497=EDGE_CURVE('',#8295,#8294,#3669,.T.);
#10498=EDGE_CURVE('',#8292,#8295,#4501,.T.);
#10499=EDGE_CURVE('',#8296,#8297,#3670,.T.);
#10500=EDGE_CURVE('',#8264,#8296,#4502,.T.);
#10501=EDGE_CURVE('',#8297,#8263,#4503,.T.);
#10502=EDGE_CURVE('',#8298,#8287,#4504,.T.);
#10503=EDGE_CURVE('',#8299,#8298,#3671,.T.);
#10504=EDGE_CURVE('',#8288,#8299,#4505,.T.);
#10505=EDGE_CURVE('',#8300,#8283,#4506,.T.);
#10506=EDGE_CURVE('',#8301,#8300,#3672,.T.);
#10507=EDGE_CURVE('',#8284,#8301,#4507,.T.);
#10508=EDGE_CURVE('',#8302,#8279,#4508,.T.);
#10509=EDGE_CURVE('',#8303,#8302,#3673,.T.);
#10510=EDGE_CURVE('',#8280,#8303,#4509,.T.);
#10511=EDGE_CURVE('',#8304,#8275,#4510,.T.);
#10512=EDGE_CURVE('',#8305,#8304,#3674,.T.);
#10513=EDGE_CURVE('',#8276,#8305,#4511,.T.);
#10514=EDGE_CURVE('',#8306,#8271,#4512,.T.);
#10515=EDGE_CURVE('',#8307,#8306,#3675,.T.);
#10516=EDGE_CURVE('',#8272,#8307,#4513,.T.);
#10517=EDGE_CURVE('',#8308,#8309,#3676,.T.);
#10518=EDGE_CURVE('',#8268,#8308,#4514,.T.);
#10519=EDGE_CURVE('',#8309,#8267,#4515,.T.);
#10520=EDGE_CURVE('',#8310,#8294,#4516,.T.);
#10521=EDGE_CURVE('',#8311,#8310,#3677,.T.);
#10522=EDGE_CURVE('',#8295,#8311,#4517,.T.);
#10523=EDGE_CURVE('',#8312,#8313,#3678,.T.);
#10524=EDGE_CURVE('',#8296,#8312,#4518,.T.);
#10525=EDGE_CURVE('',#8313,#8297,#4519,.T.);
#10526=EDGE_CURVE('',#8314,#8298,#4520,.T.);
#10527=EDGE_CURVE('',#8315,#8314,#3679,.T.);
#10528=EDGE_CURVE('',#8299,#8315,#4521,.T.);
#10529=EDGE_CURVE('',#8316,#8300,#4522,.T.);
#10530=EDGE_CURVE('',#8317,#8316,#3680,.T.);
#10531=EDGE_CURVE('',#8301,#8317,#4523,.T.);
#10532=EDGE_CURVE('',#8318,#8302,#4524,.T.);
#10533=EDGE_CURVE('',#8319,#8318,#3681,.T.);
#10534=EDGE_CURVE('',#8303,#8319,#4525,.T.);
#10535=EDGE_CURVE('',#8320,#8304,#4526,.T.);
#10536=EDGE_CURVE('',#8321,#8320,#3682,.T.);
#10537=EDGE_CURVE('',#8305,#8321,#4527,.T.);
#10538=EDGE_CURVE('',#8322,#8306,#4528,.T.);
#10539=EDGE_CURVE('',#8323,#8322,#3683,.T.);
#10540=EDGE_CURVE('',#8307,#8323,#4529,.T.);
#10541=EDGE_CURVE('',#8324,#8325,#3684,.T.);
#10542=EDGE_CURVE('',#8308,#8324,#4530,.T.);
#10543=EDGE_CURVE('',#8325,#8309,#4531,.T.);
#10544=EDGE_CURVE('',#8252,#8310,#4532,.T.);
#10545=EDGE_CURVE('',#8311,#8251,#4533,.T.);
#10546=EDGE_CURVE('',#8312,#8248,#4534,.T.);
#10547=EDGE_CURVE('',#8249,#8313,#4535,.T.);
#10548=EDGE_CURVE('',#8254,#8314,#4536,.T.);
#10549=EDGE_CURVE('',#8315,#8253,#4537,.T.);
#10550=EDGE_CURVE('',#8256,#8316,#4538,.T.);
#10551=EDGE_CURVE('',#8317,#8255,#4539,.T.);
#10552=EDGE_CURVE('',#8241,#8318,#4540,.T.);
#10553=EDGE_CURVE('',#8319,#8257,#4541,.T.);
#10554=EDGE_CURVE('',#8243,#8320,#4542,.T.);
#10555=EDGE_CURVE('',#8321,#8242,#4543,.T.);
#10556=EDGE_CURVE('',#8245,#8322,#4544,.T.);
#10557=EDGE_CURVE('',#8323,#8244,#4545,.T.);
#10558=EDGE_CURVE('',#8324,#8246,#4546,.T.);
#10559=EDGE_CURVE('',#8247,#8325,#4547,.T.);
#10560=EDGE_CURVE('',#8246,#8269,#4548,.T.);
#10561=EDGE_CURVE('',#8270,#8245,#4549,.T.);
#10562=EDGE_CURVE('',#8248,#8265,#4550,.T.);
#10563=EDGE_CURVE('',#8266,#8247,#4551,.T.);
#10564=EDGE_CURVE('',#8244,#8273,#4552,.T.);
#10565=EDGE_CURVE('',#8274,#8243,#4553,.T.);
#10566=EDGE_CURVE('',#8242,#8277,#4554,.T.);
#10567=EDGE_CURVE('',#8278,#8241,#4555,.T.);
#10568=EDGE_CURVE('',#8257,#8281,#4556,.T.);
#10569=EDGE_CURVE('',#8282,#8256,#4557,.T.);
#10570=EDGE_CURVE('',#8255,#8285,#4558,.T.);
#10571=EDGE_CURVE('',#8286,#8254,#4559,.T.);
#10572=EDGE_CURVE('',#8253,#8289,#4560,.T.);
#10573=EDGE_CURVE('',#8290,#8252,#4561,.T.);
#10574=EDGE_CURVE('',#8251,#8293,#4562,.T.);
#10575=EDGE_CURVE('',#8262,#8249,#4563,.T.);
#10576=EDGE_CURVE('',#8326,#8327,#3685,.T.);
#10577=EDGE_CURVE('',#8328,#8328,#3686,.T.);
#10578=EDGE_CURVE('',#8328,#8329,#3687,.T.);
#10579=EDGE_CURVE('',#8329,#8329,#3688,.T.);
#10580=EDGE_CURVE('',#8330,#8330,#3689,.T.);
#10581=EDGE_CURVE('',#8330,#8331,#3690,.T.);
#10582=EDGE_CURVE('',#8331,#8332,#3691,.T.);
#10583=EDGE_CURVE('',#8332,#8331,#3692,.T.);
#10584=EDGE_CURVE('',#8333,#8334,#3693,.T.);
#10585=EDGE_CURVE('',#8334,#8332,#4564,.T.);
#10586=EDGE_CURVE('',#8334,#8333,#3694,.T.);
#10587=EDGE_CURVE('',#8333,#8335,#4565,.T.);
#10588=EDGE_CURVE('',#8335,#8335,#3695,.T.);
#10589=EDGE_CURVE('',#8335,#8336,#4566,.T.);
#10590=EDGE_CURVE('',#8336,#8336,#3696,.T.);
#10591=EDGE_CURVE('',#8336,#8337,#3697,.T.);
#10592=EDGE_CURVE('',#8337,#8337,#3698,.T.);
#10593=EDGE_CURVE('',#8338,#8338,#3699,.T.);
#10594=EDGE_CURVE('',#8338,#8339,#3700,.T.);
#10595=EDGE_CURVE('',#8339,#8339,#3701,.T.);
#10596=EDGE_CURVE('',#8340,#8340,#3702,.T.);
#10597=EDGE_CURVE('',#8340,#8341,#3703,.T.);
#10598=EDGE_CURVE('',#8341,#8341,#3704,.T.);
#10599=EDGE_CURVE('',#8329,#8340,#4567,.T.);
#10600=EDGE_CURVE('',#8339,#8328,#4568,.T.);
#10601=EDGE_CURVE('',#8342,#8342,#3705,.T.);
#10602=EDGE_CURVE('',#8342,#8343,#3706,.T.);
#10603=EDGE_CURVE('',#8343,#8343,#3707,.T.);
#10604=EDGE_CURVE('',#8344,#8344,#3708,.T.);
#10605=EDGE_CURVE('',#8344,#8345,#4569,.T.);
#10606=EDGE_CURVE('',#8345,#8345,#3709,.T.);
#10607=EDGE_CURVE('',#8345,#8346,#3710,.T.);
#10608=EDGE_CURVE('',#8346,#8346,#3711,.T.);
#10609=EDGE_CURVE('',#8346,#8347,#4570,.T.);
#10610=EDGE_CURVE('',#8347,#8347,#3712,.T.);
#10611=EDGE_CURVE('',#8348,#8349,#3713,.T.);
#10612=EDGE_CURVE('',#8349,#8350,#4571,.T.);
#10613=EDGE_CURVE('',#8350,#8350,#3714,.T.);
#10614=EDGE_CURVE('',#8349,#8348,#3715,.T.);
#10615=EDGE_CURVE('',#8348,#8344,#3716,.T.);
#10616=EDGE_CURVE('',#8351,#8351,#3717,.T.);
#10617=EDGE_CURVE('',#8351,#8342,#4572,.T.);
#10618=EDGE_CURVE('',#8343,#8352,#4573,.T.);
#10619=EDGE_CURVE('',#8352,#8352,#3718,.T.);
#10620=EDGE_CURVE('',#8353,#8354,#3719,.T.);
#10621=EDGE_CURVE('',#8355,#8356,#3720,.T.);
#10622=EDGE_CURVE('',#8357,#8358,#3721,.T.);
#10623=EDGE_CURVE('',#8359,#8360,#3722,.T.);
#10624=EDGE_CURVE('',#8361,#8362,#3723,.T.);
#10625=EDGE_CURVE('',#8363,#8364,#3724,.T.);
#10626=EDGE_CURVE('',#8365,#8366,#3725,.T.);
#10627=EDGE_CURVE('',#8367,#8368,#3726,.T.);
#10628=EDGE_CURVE('',#8368,#8367,#3727,.T.);
#10629=EDGE_CURVE('',#8368,#8369,#3728,.T.);
#10630=EDGE_CURVE('',#8370,#8369,#3729,.T.);
#10631=EDGE_CURVE('',#8369,#8370,#3730,.T.);
#10632=EDGE_CURVE('',#8371,#8371,#3731,.T.);
#10633=EDGE_CURVE('',#8371,#8372,#4574,.T.);
#10634=EDGE_CURVE('',#8372,#8372,#3732,.T.);
#10635=EDGE_CURVE('',#8373,#8373,#3733,.T.);
#10636=EDGE_CURVE('',#8373,#8371,#3734,.T.);
#10637=EDGE_CURVE('',#8374,#8374,#3735,.T.);
#10638=EDGE_CURVE('',#8374,#8375,#3736,.T.);
#10639=EDGE_CURVE('',#8375,#8375,#3737,.T.);
#10640=EDGE_CURVE('',#8376,#8376,#3738,.T.);
#10641=EDGE_CURVE('',#8376,#8374,#4575,.T.);
#10642=EDGE_CURVE('',#8377,#8378,#3739,.T.);
#10643=EDGE_CURVE('',#8379,#8377,#3740,.T.);
#10644=EDGE_CURVE('',#8380,#8379,#3741,.T.);
#10645=EDGE_CURVE('',#8381,#8380,#3742,.T.);
#10646=EDGE_CURVE('',#8382,#8381,#3743,.T.);
#10647=EDGE_CURVE('',#8383,#8382,#3744,.T.);
#10648=EDGE_CURVE('',#8384,#8383,#3745,.T.);
#10649=EDGE_CURVE('',#8385,#8384,#3746,.T.);
#10650=EDGE_CURVE('',#8386,#8385,#3747,.T.);
#10651=EDGE_CURVE('',#8386,#8376,#3748,.T.);
#10652=EDGE_CURVE('',#8387,#8386,#3749,.T.);
#10653=EDGE_CURVE('',#8388,#8387,#3750,.T.);
#10654=EDGE_CURVE('',#8389,#8388,#3751,.T.);
#10655=EDGE_CURVE('',#8390,#8389,#3752,.T.);
#10656=EDGE_CURVE('',#8391,#8390,#3753,.T.);
#10657=EDGE_CURVE('',#8392,#8391,#3754,.T.);
#10658=EDGE_CURVE('',#8393,#8392,#3755,.T.);
#10659=EDGE_CURVE('',#8378,#8393,#3756,.T.);
#10660=EDGE_CURVE('',#8394,#8394,#3757,.T.);
#10661=EDGE_CURVE('',#8394,#8395,#3758,.T.);
#10662=EDGE_CURVE('',#8395,#8395,#3759,.T.);
#10663=EDGE_CURVE('',#8395,#8370,#4576,.T.);
#10664=EDGE_CURVE('',#8367,#8396,#3760,.T.);
#10665=EDGE_CURVE('',#8397,#8396,#3761,.T.);
#10666=EDGE_CURVE('',#8397,#8398,#3762,.T.);
#10667=EDGE_CURVE('',#8398,#8399,#3763,.T.);
#10668=EDGE_CURVE('',#8399,#8400,#3764,.T.);
#10669=EDGE_CURVE('',#8401,#8400,#3765,.T.);
#10670=EDGE_CURVE('',#8401,#8402,#3766,.T.);
#10671=EDGE_CURVE('',#8402,#8403,#3767,.T.);
#10672=EDGE_CURVE('',#8403,#8404,#3768,.T.);
#10673=EDGE_CURVE('',#8405,#8404,#3769,.T.);
#10674=EDGE_CURVE('',#8405,#8406,#3770,.T.);
#10675=EDGE_CURVE('',#8406,#8407,#3771,.T.);
#10676=EDGE_CURVE('',#8407,#8408,#3772,.T.);
#10677=EDGE_CURVE('',#8409,#8408,#3773,.T.);
#10678=EDGE_CURVE('',#8409,#8410,#3774,.T.);
#10679=EDGE_CURVE('',#8410,#8411,#3775,.T.);
#10680=EDGE_CURVE('',#8411,#8412,#3776,.T.);
#10681=EDGE_CURVE('',#8413,#8412,#3777,.T.);
#10682=EDGE_CURVE('',#8413,#8414,#3778,.T.);
#10683=EDGE_CURVE('',#8414,#8415,#3779,.T.);
#10684=EDGE_CURVE('',#8415,#8416,#3780,.T.);
#10685=EDGE_CURVE('',#8417,#8416,#3781,.T.);
#10686=EDGE_CURVE('',#8417,#8418,#3782,.T.);
#10687=EDGE_CURVE('',#8418,#8419,#3783,.T.);
#10688=EDGE_CURVE('',#8419,#8420,#3784,.T.);
#10689=EDGE_CURVE('',#8421,#8420,#3785,.T.);
#10690=EDGE_CURVE('',#8421,#8422,#3786,.T.);
#10691=EDGE_CURVE('',#8422,#8423,#3787,.T.);
#10692=EDGE_CURVE('',#8423,#8424,#3788,.T.);
#10693=EDGE_CURVE('',#8425,#8424,#3789,.T.);
#10694=EDGE_CURVE('',#8425,#8426,#3790,.T.);
#10695=EDGE_CURVE('',#8426,#8427,#3791,.T.);
#10696=EDGE_CURVE('',#8427,#8428,#3792,.T.);
#10697=EDGE_CURVE('',#8396,#8428,#3793,.T.);
#10698=EDGE_CURVE('',#8398,#8429,#4577,.T.);
#10699=EDGE_CURVE('',#8429,#8430,#3794,.T.);
#10700=EDGE_CURVE('',#8430,#8399,#4578,.T.);
#10701=EDGE_CURVE('',#8431,#8432,#3795,.T.);
#10702=EDGE_CURVE('',#8432,#8427,#4579,.T.);
#10703=EDGE_CURVE('',#8426,#8431,#4580,.T.);
#10704=EDGE_CURVE('',#8402,#8433,#4581,.T.);
#10705=EDGE_CURVE('',#8433,#8434,#3796,.T.);
#10706=EDGE_CURVE('',#8434,#8403,#4582,.T.);
#10707=EDGE_CURVE('',#8406,#8435,#4583,.T.);
#10708=EDGE_CURVE('',#8435,#8436,#3797,.T.);
#10709=EDGE_CURVE('',#8436,#8407,#4584,.T.);
#10710=EDGE_CURVE('',#8410,#8437,#4585,.T.);
#10711=EDGE_CURVE('',#8437,#8438,#3798,.T.);
#10712=EDGE_CURVE('',#8438,#8411,#4586,.T.);
#10713=EDGE_CURVE('',#8414,#8439,#4587,.T.);
#10714=EDGE_CURVE('',#8439,#8440,#3799,.T.);
#10715=EDGE_CURVE('',#8440,#8415,#4588,.T.);
#10716=EDGE_CURVE('',#8418,#8441,#4589,.T.);
#10717=EDGE_CURVE('',#8441,#8442,#3800,.T.);
#10718=EDGE_CURVE('',#8442,#8419,#4590,.T.);
#10719=EDGE_CURVE('',#8443,#8444,#3801,.T.);
#10720=EDGE_CURVE('',#8444,#8423,#4591,.T.);
#10721=EDGE_CURVE('',#8422,#8443,#4592,.T.);
#10722=EDGE_CURVE('',#8429,#8445,#4593,.T.);
#10723=EDGE_CURVE('',#8445,#8446,#3802,.T.);
#10724=EDGE_CURVE('',#8446,#8430,#4594,.T.);
#10725=EDGE_CURVE('',#8447,#8448,#3803,.T.);
#10726=EDGE_CURVE('',#8448,#8432,#4595,.T.);
#10727=EDGE_CURVE('',#8431,#8447,#4596,.T.);
#10728=EDGE_CURVE('',#8433,#8449,#4597,.T.);
#10729=EDGE_CURVE('',#8449,#8450,#3804,.T.);
#10730=EDGE_CURVE('',#8450,#8434,#4598,.T.);
#10731=EDGE_CURVE('',#8435,#8451,#4599,.T.);
#10732=EDGE_CURVE('',#8451,#8452,#3805,.T.);
#10733=EDGE_CURVE('',#8452,#8436,#4600,.T.);
#10734=EDGE_CURVE('',#8437,#8453,#4601,.T.);
#10735=EDGE_CURVE('',#8453,#8454,#3806,.T.);
#10736=EDGE_CURVE('',#8454,#8438,#4602,.T.);
#10737=EDGE_CURVE('',#8439,#8455,#4603,.T.);
#10738=EDGE_CURVE('',#8455,#8456,#3807,.T.);
#10739=EDGE_CURVE('',#8456,#8440,#4604,.T.);
#10740=EDGE_CURVE('',#8441,#8457,#4605,.T.);
#10741=EDGE_CURVE('',#8457,#8458,#3808,.T.);
#10742=EDGE_CURVE('',#8458,#8442,#4606,.T.);
#10743=EDGE_CURVE('',#8459,#8460,#3809,.T.);
#10744=EDGE_CURVE('',#8460,#8444,#4607,.T.);
#10745=EDGE_CURVE('',#8443,#8459,#4608,.T.);
#10746=EDGE_CURVE('',#8445,#8385,#4609,.T.);
#10747=EDGE_CURVE('',#8384,#8446,#4610,.T.);
#10748=EDGE_CURVE('',#8387,#8448,#4611,.T.);
#10749=EDGE_CURVE('',#8447,#8388,#4612,.T.);
#10750=EDGE_CURVE('',#8449,#8383,#4613,.T.);
#10751=EDGE_CURVE('',#8382,#8450,#4614,.T.);
#10752=EDGE_CURVE('',#8451,#8381,#4615,.T.);
#10753=EDGE_CURVE('',#8380,#8452,#4616,.T.);
#10754=EDGE_CURVE('',#8453,#8379,#4617,.T.);
#10755=EDGE_CURVE('',#8377,#8454,#4618,.T.);
#10756=EDGE_CURVE('',#8455,#8378,#4619,.T.);
#10757=EDGE_CURVE('',#8393,#8456,#4620,.T.);
#10758=EDGE_CURVE('',#8457,#8392,#4621,.T.);
#10759=EDGE_CURVE('',#8391,#8458,#4622,.T.);
#10760=EDGE_CURVE('',#8389,#8460,#4623,.T.);
#10761=EDGE_CURVE('',#8459,#8390,#4624,.T.);
#10762=EDGE_CURVE('',#8390,#8421,#4625,.T.);
#10763=EDGE_CURVE('',#8420,#8391,#4626,.T.);
#10764=EDGE_CURVE('',#8388,#8425,#4627,.T.);
#10765=EDGE_CURVE('',#8424,#8389,#4628,.T.);
#10766=EDGE_CURVE('',#8392,#8417,#4629,.T.);
#10767=EDGE_CURVE('',#8416,#8393,#4630,.T.);
#10768=EDGE_CURVE('',#8378,#8413,#4631,.T.);
#10769=EDGE_CURVE('',#8412,#8377,#4632,.T.);
#10770=EDGE_CURVE('',#8379,#8409,#4633,.T.);
#10771=EDGE_CURVE('',#8408,#8380,#4634,.T.);
#10772=EDGE_CURVE('',#8381,#8405,#4635,.T.);
#10773=EDGE_CURVE('',#8404,#8382,#4636,.T.);
#10774=EDGE_CURVE('',#8383,#8401,#4637,.T.);
#10775=EDGE_CURVE('',#8400,#8384,#4638,.T.);
#10776=EDGE_CURVE('',#8385,#8397,#4639,.T.);
#10777=EDGE_CURVE('',#8428,#8387,#4640,.T.);
#14091=ORIENTED_EDGE('',*,*,#10429,.T.);
#14092=ORIENTED_EDGE('',*,*,#10430,.T.);
#14093=ORIENTED_EDGE('',*,*,#10431,.F.);
#14094=ORIENTED_EDGE('',*,*,#10430,.F.);
#14095=ORIENTED_EDGE('',*,*,#10432,.T.);
#14096=ORIENTED_EDGE('',*,*,#10433,.T.);
#14097=ORIENTED_EDGE('',*,*,#10429,.F.);
#14098=ORIENTED_EDGE('',*,*,#10433,.F.);
#14099=ORIENTED_EDGE('',*,*,#10434,.T.);
#14100=ORIENTED_EDGE('',*,*,#10435,.T.);
#14101=ORIENTED_EDGE('',*,*,#10436,.F.);
#14102=ORIENTED_EDGE('',*,*,#10435,.F.);
#14103=ORIENTED_EDGE('',*,*,#10437,.T.);
#14104=ORIENTED_EDGE('',*,*,#10438,.T.);
#14105=ORIENTED_EDGE('',*,*,#10434,.F.);
#14106=ORIENTED_EDGE('',*,*,#10438,.F.);
#14107=ORIENTED_EDGE('',*,*,#10439,.T.);
#14108=ORIENTED_EDGE('',*,*,#10440,.T.);
#14109=ORIENTED_EDGE('',*,*,#10441,.T.);
#14110=ORIENTED_EDGE('',*,*,#10442,.T.);
#14111=ORIENTED_EDGE('',*,*,#10443,.T.);
#14112=ORIENTED_EDGE('',*,*,#10444,.T.);
#14113=ORIENTED_EDGE('',*,*,#10445,.T.);
#14114=ORIENTED_EDGE('',*,*,#10446,.T.);
#14115=ORIENTED_EDGE('',*,*,#10447,.T.);
#14116=ORIENTED_EDGE('',*,*,#10448,.T.);
#14117=ORIENTED_EDGE('',*,*,#10437,.F.);
#14118=ORIENTED_EDGE('',*,*,#10448,.F.);
#14119=ORIENTED_EDGE('',*,*,#10449,.T.);
#14120=ORIENTED_EDGE('',*,*,#10450,.T.);
#14121=ORIENTED_EDGE('',*,*,#10451,.T.);
#14122=ORIENTED_EDGE('',*,*,#10452,.T.);
#14123=ORIENTED_EDGE('',*,*,#10453,.T.);
#14124=ORIENTED_EDGE('',*,*,#10454,.T.);
#14125=ORIENTED_EDGE('',*,*,#10455,.T.);
#14126=ORIENTED_EDGE('',*,*,#10456,.T.);
#14127=ORIENTED_EDGE('',*,*,#10457,.T.);
#14128=ORIENTED_EDGE('',*,*,#10458,.T.);
#14129=ORIENTED_EDGE('',*,*,#10459,.F.);
#14130=ORIENTED_EDGE('',*,*,#10458,.F.);
#14131=ORIENTED_EDGE('',*,*,#10460,.T.);
#14132=ORIENTED_EDGE('',*,*,#10461,.T.);
#14133=ORIENTED_EDGE('',*,*,#10457,.F.);
#14134=ORIENTED_EDGE('',*,*,#10461,.F.);
#14135=ORIENTED_EDGE('',*,*,#10459,.T.);
#14136=ORIENTED_EDGE('',*,*,#10462,.T.);
#14137=ORIENTED_EDGE('',*,*,#10463,.T.);
#14138=ORIENTED_EDGE('',*,*,#10464,.F.);
#14139=ORIENTED_EDGE('',*,*,#10465,.F.);
#14140=ORIENTED_EDGE('',*,*,#10466,.F.);
#14141=ORIENTED_EDGE('',*,*,#10467,.T.);
#14142=ORIENTED_EDGE('',*,*,#10468,.F.);
#14143=ORIENTED_EDGE('',*,*,#10469,.F.);
#14144=ORIENTED_EDGE('',*,*,#10470,.F.);
#14145=ORIENTED_EDGE('',*,*,#10471,.T.);
#14146=ORIENTED_EDGE('',*,*,#10472,.F.);
#14147=ORIENTED_EDGE('',*,*,#10473,.F.);
#14148=ORIENTED_EDGE('',*,*,#10474,.F.);
#14149=ORIENTED_EDGE('',*,*,#10475,.T.);
#14150=ORIENTED_EDGE('',*,*,#10476,.F.);
#14151=ORIENTED_EDGE('',*,*,#10477,.F.);
#14152=ORIENTED_EDGE('',*,*,#10478,.F.);
#14153=ORIENTED_EDGE('',*,*,#10479,.T.);
#14154=ORIENTED_EDGE('',*,*,#10480,.F.);
#14155=ORIENTED_EDGE('',*,*,#10481,.F.);
#14156=ORIENTED_EDGE('',*,*,#10482,.F.);
#14157=ORIENTED_EDGE('',*,*,#10483,.T.);
#14158=ORIENTED_EDGE('',*,*,#10484,.F.);
#14159=ORIENTED_EDGE('',*,*,#10485,.F.);
#14160=ORIENTED_EDGE('',*,*,#10486,.F.);
#14161=ORIENTED_EDGE('',*,*,#10487,.T.);
#14162=ORIENTED_EDGE('',*,*,#10488,.F.);
#14163=ORIENTED_EDGE('',*,*,#10489,.F.);
#14164=ORIENTED_EDGE('',*,*,#10490,.F.);
#14165=ORIENTED_EDGE('',*,*,#10491,.T.);
#14166=ORIENTED_EDGE('',*,*,#10492,.F.);
#14167=ORIENTED_EDGE('',*,*,#10493,.F.);
#14168=ORIENTED_EDGE('',*,*,#10494,.F.);
#14169=ORIENTED_EDGE('',*,*,#10495,.T.);
#14170=ORIENTED_EDGE('',*,*,#10462,.F.);
#14171=ORIENTED_EDGE('',*,*,#10493,.T.);
#14172=ORIENTED_EDGE('',*,*,#10496,.F.);
#14173=ORIENTED_EDGE('',*,*,#10497,.F.);
#14174=ORIENTED_EDGE('',*,*,#10498,.F.);
#14175=ORIENTED_EDGE('',*,*,#10499,.F.);
#14176=ORIENTED_EDGE('',*,*,#10500,.F.);
#14177=ORIENTED_EDGE('',*,*,#10465,.T.);
#14178=ORIENTED_EDGE('',*,*,#10501,.F.);
#14179=ORIENTED_EDGE('',*,*,#10489,.T.);
#14180=ORIENTED_EDGE('',*,*,#10502,.F.);
#14181=ORIENTED_EDGE('',*,*,#10503,.F.);
#14182=ORIENTED_EDGE('',*,*,#10504,.F.);
#14183=ORIENTED_EDGE('',*,*,#10485,.T.);
#14184=ORIENTED_EDGE('',*,*,#10505,.F.);
#14185=ORIENTED_EDGE('',*,*,#10506,.F.);
#14186=ORIENTED_EDGE('',*,*,#10507,.F.);
#14187=ORIENTED_EDGE('',*,*,#10481,.T.);
#14188=ORIENTED_EDGE('',*,*,#10508,.F.);
#14189=ORIENTED_EDGE('',*,*,#10509,.F.);
#14190=ORIENTED_EDGE('',*,*,#10510,.F.);
#14191=ORIENTED_EDGE('',*,*,#10477,.T.);
#14192=ORIENTED_EDGE('',*,*,#10511,.F.);
#14193=ORIENTED_EDGE('',*,*,#10512,.F.);
#14194=ORIENTED_EDGE('',*,*,#10513,.F.);
#14195=ORIENTED_EDGE('',*,*,#10473,.T.);
#14196=ORIENTED_EDGE('',*,*,#10514,.F.);
#14197=ORIENTED_EDGE('',*,*,#10515,.F.);
#14198=ORIENTED_EDGE('',*,*,#10516,.F.);
#14199=ORIENTED_EDGE('',*,*,#10517,.F.);
#14200=ORIENTED_EDGE('',*,*,#10518,.F.);
#14201=ORIENTED_EDGE('',*,*,#10469,.T.);
#14202=ORIENTED_EDGE('',*,*,#10519,.F.);
#14203=ORIENTED_EDGE('',*,*,#10497,.T.);
#14204=ORIENTED_EDGE('',*,*,#10520,.F.);
#14205=ORIENTED_EDGE('',*,*,#10521,.F.);
#14206=ORIENTED_EDGE('',*,*,#10522,.F.);
#14207=ORIENTED_EDGE('',*,*,#10523,.F.);
#14208=ORIENTED_EDGE('',*,*,#10524,.F.);
#14209=ORIENTED_EDGE('',*,*,#10499,.T.);
#14210=ORIENTED_EDGE('',*,*,#10525,.F.);
#14211=ORIENTED_EDGE('',*,*,#10503,.T.);
#14212=ORIENTED_EDGE('',*,*,#10526,.F.);
#14213=ORIENTED_EDGE('',*,*,#10527,.F.);
#14214=ORIENTED_EDGE('',*,*,#10528,.F.);
#14215=ORIENTED_EDGE('',*,*,#10506,.T.);
#14216=ORIENTED_EDGE('',*,*,#10529,.F.);
#14217=ORIENTED_EDGE('',*,*,#10530,.F.);
#14218=ORIENTED_EDGE('',*,*,#10531,.F.);
#14219=ORIENTED_EDGE('',*,*,#10509,.T.);
#14220=ORIENTED_EDGE('',*,*,#10532,.F.);
#14221=ORIENTED_EDGE('',*,*,#10533,.F.);
#14222=ORIENTED_EDGE('',*,*,#10534,.F.);
#14223=ORIENTED_EDGE('',*,*,#10512,.T.);
#14224=ORIENTED_EDGE('',*,*,#10535,.F.);
#14225=ORIENTED_EDGE('',*,*,#10536,.F.);
#14226=ORIENTED_EDGE('',*,*,#10537,.F.);
#14227=ORIENTED_EDGE('',*,*,#10515,.T.);
#14228=ORIENTED_EDGE('',*,*,#10538,.F.);
#14229=ORIENTED_EDGE('',*,*,#10539,.F.);
#14230=ORIENTED_EDGE('',*,*,#10540,.F.);
#14231=ORIENTED_EDGE('',*,*,#10541,.F.);
#14232=ORIENTED_EDGE('',*,*,#10542,.F.);
#14233=ORIENTED_EDGE('',*,*,#10517,.T.);
#14234=ORIENTED_EDGE('',*,*,#10543,.F.);
#14235=ORIENTED_EDGE('',*,*,#10521,.T.);
#14236=ORIENTED_EDGE('',*,*,#10544,.F.);
#14237=ORIENTED_EDGE('',*,*,#10450,.F.);
#14238=ORIENTED_EDGE('',*,*,#10545,.F.);
#14239=ORIENTED_EDGE('',*,*,#10446,.F.);
#14240=ORIENTED_EDGE('',*,*,#10546,.F.);
#14241=ORIENTED_EDGE('',*,*,#10523,.T.);
#14242=ORIENTED_EDGE('',*,*,#10547,.F.);
#14243=ORIENTED_EDGE('',*,*,#10527,.T.);
#14244=ORIENTED_EDGE('',*,*,#10548,.F.);
#14245=ORIENTED_EDGE('',*,*,#10452,.F.);
#14246=ORIENTED_EDGE('',*,*,#10549,.F.);
#14247=ORIENTED_EDGE('',*,*,#10530,.T.);
#14248=ORIENTED_EDGE('',*,*,#10550,.F.);
#14249=ORIENTED_EDGE('',*,*,#10454,.F.);
#14250=ORIENTED_EDGE('',*,*,#10551,.F.);
#14251=ORIENTED_EDGE('',*,*,#10533,.T.);
#14252=ORIENTED_EDGE('',*,*,#10552,.F.);
#14253=ORIENTED_EDGE('',*,*,#10456,.F.);
#14254=ORIENTED_EDGE('',*,*,#10553,.F.);
#14255=ORIENTED_EDGE('',*,*,#10536,.T.);
#14256=ORIENTED_EDGE('',*,*,#10554,.F.);
#14257=ORIENTED_EDGE('',*,*,#10440,.F.);
#14258=ORIENTED_EDGE('',*,*,#10555,.F.);
#14259=ORIENTED_EDGE('',*,*,#10539,.T.);
#14260=ORIENTED_EDGE('',*,*,#10556,.F.);
#14261=ORIENTED_EDGE('',*,*,#10442,.F.);
#14262=ORIENTED_EDGE('',*,*,#10557,.F.);
#14263=ORIENTED_EDGE('',*,*,#10444,.F.);
#14264=ORIENTED_EDGE('',*,*,#10558,.F.);
#14265=ORIENTED_EDGE('',*,*,#10541,.T.);
#14266=ORIENTED_EDGE('',*,*,#10559,.F.);
#14267=ORIENTED_EDGE('',*,*,#10436,.T.);
#14268=ORIENTED_EDGE('',*,*,#10432,.F.);
#14269=ORIENTED_EDGE('',*,*,#10460,.F.);
#14270=ORIENTED_EDGE('',*,*,#10431,.T.);
#14271=ORIENTED_EDGE('',*,*,#10560,.T.);
#14272=ORIENTED_EDGE('',*,*,#10470,.T.);
#14273=ORIENTED_EDGE('',*,*,#10518,.T.);
#14274=ORIENTED_EDGE('',*,*,#10542,.T.);
#14275=ORIENTED_EDGE('',*,*,#10558,.T.);
#14276=ORIENTED_EDGE('',*,*,#10514,.T.);
#14277=ORIENTED_EDGE('',*,*,#10472,.T.);
#14278=ORIENTED_EDGE('',*,*,#10561,.T.);
#14279=ORIENTED_EDGE('',*,*,#10556,.T.);
#14280=ORIENTED_EDGE('',*,*,#10538,.T.);
#14281=ORIENTED_EDGE('',*,*,#10471,.F.);
#14282=ORIENTED_EDGE('',*,*,#10560,.F.);
#14283=ORIENTED_EDGE('',*,*,#10443,.F.);
#14284=ORIENTED_EDGE('',*,*,#10561,.F.);
#14285=ORIENTED_EDGE('',*,*,#10562,.T.);
#14286=ORIENTED_EDGE('',*,*,#10466,.T.);
#14287=ORIENTED_EDGE('',*,*,#10500,.T.);
#14288=ORIENTED_EDGE('',*,*,#10524,.T.);
#14289=ORIENTED_EDGE('',*,*,#10546,.T.);
#14290=ORIENTED_EDGE('',*,*,#10519,.T.);
#14291=ORIENTED_EDGE('',*,*,#10468,.T.);
#14292=ORIENTED_EDGE('',*,*,#10563,.T.);
#14293=ORIENTED_EDGE('',*,*,#10559,.T.);
#14294=ORIENTED_EDGE('',*,*,#10543,.T.);
#14295=ORIENTED_EDGE('',*,*,#10467,.F.);
#14296=ORIENTED_EDGE('',*,*,#10562,.F.);
#14297=ORIENTED_EDGE('',*,*,#10445,.F.);
#14298=ORIENTED_EDGE('',*,*,#10563,.F.);
#14299=ORIENTED_EDGE('',*,*,#10564,.T.);
#14300=ORIENTED_EDGE('',*,*,#10474,.T.);
#14301=ORIENTED_EDGE('',*,*,#10516,.T.);
#14302=ORIENTED_EDGE('',*,*,#10540,.T.);
#14303=ORIENTED_EDGE('',*,*,#10557,.T.);
#14304=ORIENTED_EDGE('',*,*,#10511,.T.);
#14305=ORIENTED_EDGE('',*,*,#10476,.T.);
#14306=ORIENTED_EDGE('',*,*,#10565,.T.);
#14307=ORIENTED_EDGE('',*,*,#10554,.T.);
#14308=ORIENTED_EDGE('',*,*,#10535,.T.);
#14309=ORIENTED_EDGE('',*,*,#10475,.F.);
#14310=ORIENTED_EDGE('',*,*,#10564,.F.);
#14311=ORIENTED_EDGE('',*,*,#10441,.F.);
#14312=ORIENTED_EDGE('',*,*,#10565,.F.);
#14313=ORIENTED_EDGE('',*,*,#10566,.T.);
#14314=ORIENTED_EDGE('',*,*,#10478,.T.);
#14315=ORIENTED_EDGE('',*,*,#10513,.T.);
#14316=ORIENTED_EDGE('',*,*,#10537,.T.);
#14317=ORIENTED_EDGE('',*,*,#10555,.T.);
#14318=ORIENTED_EDGE('',*,*,#10508,.T.);
#14319=ORIENTED_EDGE('',*,*,#10480,.T.);
#14320=ORIENTED_EDGE('',*,*,#10567,.T.);
#14321=ORIENTED_EDGE('',*,*,#10552,.T.);
#14322=ORIENTED_EDGE('',*,*,#10532,.T.);
#14323=ORIENTED_EDGE('',*,*,#10479,.F.);
#14324=ORIENTED_EDGE('',*,*,#10566,.F.);
#14325=ORIENTED_EDGE('',*,*,#10439,.F.);
#14326=ORIENTED_EDGE('',*,*,#10567,.F.);
#14327=ORIENTED_EDGE('',*,*,#10568,.T.);
#14328=ORIENTED_EDGE('',*,*,#10482,.T.);
#14329=ORIENTED_EDGE('',*,*,#10510,.T.);
#14330=ORIENTED_EDGE('',*,*,#10534,.T.);
#14331=ORIENTED_EDGE('',*,*,#10553,.T.);
#14332=ORIENTED_EDGE('',*,*,#10505,.T.);
#14333=ORIENTED_EDGE('',*,*,#10484,.T.);
#14334=ORIENTED_EDGE('',*,*,#10569,.T.);
#14335=ORIENTED_EDGE('',*,*,#10550,.T.);
#14336=ORIENTED_EDGE('',*,*,#10529,.T.);
#14337=ORIENTED_EDGE('',*,*,#10483,.F.);
#14338=ORIENTED_EDGE('',*,*,#10568,.F.);
#14339=ORIENTED_EDGE('',*,*,#10455,.F.);
#14340=ORIENTED_EDGE('',*,*,#10569,.F.);
#14341=ORIENTED_EDGE('',*,*,#10570,.T.);
#14342=ORIENTED_EDGE('',*,*,#10486,.T.);
#14343=ORIENTED_EDGE('',*,*,#10507,.T.);
#14344=ORIENTED_EDGE('',*,*,#10531,.T.);
#14345=ORIENTED_EDGE('',*,*,#10551,.T.);
#14346=ORIENTED_EDGE('',*,*,#10502,.T.);
#14347=ORIENTED_EDGE('',*,*,#10488,.T.);
#14348=ORIENTED_EDGE('',*,*,#10571,.T.);
#14349=ORIENTED_EDGE('',*,*,#10548,.T.);
#14350=ORIENTED_EDGE('',*,*,#10526,.T.);
#14351=ORIENTED_EDGE('',*,*,#10487,.F.);
#14352=ORIENTED_EDGE('',*,*,#10570,.F.);
#14353=ORIENTED_EDGE('',*,*,#10453,.F.);
#14354=ORIENTED_EDGE('',*,*,#10571,.F.);
#14355=ORIENTED_EDGE('',*,*,#10572,.T.);
#14356=ORIENTED_EDGE('',*,*,#10490,.T.);
#14357=ORIENTED_EDGE('',*,*,#10504,.T.);
#14358=ORIENTED_EDGE('',*,*,#10528,.T.);
#14359=ORIENTED_EDGE('',*,*,#10549,.T.);
#14360=ORIENTED_EDGE('',*,*,#10496,.T.);
#14361=ORIENTED_EDGE('',*,*,#10492,.T.);
#14362=ORIENTED_EDGE('',*,*,#10573,.T.);
#14363=ORIENTED_EDGE('',*,*,#10544,.T.);
#14364=ORIENTED_EDGE('',*,*,#10520,.T.);
#14365=ORIENTED_EDGE('',*,*,#10491,.F.);
#14366=ORIENTED_EDGE('',*,*,#10572,.F.);
#14367=ORIENTED_EDGE('',*,*,#10451,.F.);
#14368=ORIENTED_EDGE('',*,*,#10573,.F.);
#14369=ORIENTED_EDGE('',*,*,#10574,.T.);
#14370=ORIENTED_EDGE('',*,*,#10494,.T.);
#14371=ORIENTED_EDGE('',*,*,#10498,.T.);
#14372=ORIENTED_EDGE('',*,*,#10522,.T.);
#14373=ORIENTED_EDGE('',*,*,#10545,.T.);
#14374=ORIENTED_EDGE('',*,*,#10501,.T.);
#14375=ORIENTED_EDGE('',*,*,#10464,.T.);
#14376=ORIENTED_EDGE('',*,*,#10575,.T.);
#14377=ORIENTED_EDGE('',*,*,#10547,.T.);
#14378=ORIENTED_EDGE('',*,*,#10525,.T.);
#14379=ORIENTED_EDGE('',*,*,#10495,.F.);
#14380=ORIENTED_EDGE('',*,*,#10574,.F.);
#14381=ORIENTED_EDGE('',*,*,#10449,.F.);
#14382=ORIENTED_EDGE('',*,*,#10447,.F.);
#14383=ORIENTED_EDGE('',*,*,#10575,.F.);
#14384=ORIENTED_EDGE('',*,*,#10463,.F.);
#14385=ORIENTED_EDGE('',*,*,#10576,.T.);
#14386=ORIENTED_EDGE('',*,*,#10576,.F.);
#14387=ORIENTED_EDGE('',*,*,#10577,.T.);
#14388=ORIENTED_EDGE('',*,*,#10578,.T.);
#14389=ORIENTED_EDGE('',*,*,#10579,.T.);
#14390=ORIENTED_EDGE('',*,*,#10578,.F.);
#14391=ORIENTED_EDGE('',*,*,#10580,.F.);
#14392=ORIENTED_EDGE('',*,*,#10581,.T.);
#14393=ORIENTED_EDGE('',*,*,#10582,.T.);
#14394=ORIENTED_EDGE('',*,*,#10583,.T.);
#14395=ORIENTED_EDGE('',*,*,#10581,.F.);
#14396=ORIENTED_EDGE('',*,*,#10584,.T.);
#14397=ORIENTED_EDGE('',*,*,#10585,.T.);
#14398=ORIENTED_EDGE('',*,*,#10582,.F.);
#14399=ORIENTED_EDGE('',*,*,#10583,.F.);
#14400=ORIENTED_EDGE('',*,*,#10585,.F.);
#14401=ORIENTED_EDGE('',*,*,#10586,.T.);
#14402=ORIENTED_EDGE('',*,*,#10584,.F.);
#14403=ORIENTED_EDGE('',*,*,#10587,.T.);
#14404=ORIENTED_EDGE('',*,*,#10588,.T.);
#14405=ORIENTED_EDGE('',*,*,#10587,.F.);
#14406=ORIENTED_EDGE('',*,*,#10586,.F.);
#14407=ORIENTED_EDGE('',*,*,#10588,.F.);
#14408=ORIENTED_EDGE('',*,*,#10589,.T.);
#14409=ORIENTED_EDGE('',*,*,#10590,.T.);
#14410=ORIENTED_EDGE('',*,*,#10589,.F.);
#14411=ORIENTED_EDGE('',*,*,#10590,.F.);
#14412=ORIENTED_EDGE('',*,*,#10591,.T.);
#14413=ORIENTED_EDGE('',*,*,#10592,.T.);
#14414=ORIENTED_EDGE('',*,*,#10591,.F.);
#14415=ORIENTED_EDGE('',*,*,#10593,.F.);
#14416=ORIENTED_EDGE('',*,*,#10594,.T.);
#14417=ORIENTED_EDGE('',*,*,#10595,.T.);
#14418=ORIENTED_EDGE('',*,*,#10594,.F.);
#14419=ORIENTED_EDGE('',*,*,#10596,.F.);
#14420=ORIENTED_EDGE('',*,*,#10597,.T.);
#14421=ORIENTED_EDGE('',*,*,#10598,.T.);
#14422=ORIENTED_EDGE('',*,*,#10597,.F.);
#14423=ORIENTED_EDGE('',*,*,#10579,.F.);
#14424=ORIENTED_EDGE('',*,*,#10599,.T.);
#14425=ORIENTED_EDGE('',*,*,#10596,.T.);
#14426=ORIENTED_EDGE('',*,*,#10599,.F.);
#14427=ORIENTED_EDGE('',*,*,#10595,.F.);
#14428=ORIENTED_EDGE('',*,*,#10600,.T.);
#14429=ORIENTED_EDGE('',*,*,#10577,.F.);
#14430=ORIENTED_EDGE('',*,*,#10600,.F.);
#14431=ORIENTED_EDGE('',*,*,#10593,.T.);
#14432=ORIENTED_EDGE('',*,*,#10592,.F.);
#14433=ORIENTED_EDGE('',*,*,#10598,.F.);
#14434=ORIENTED_EDGE('',*,*,#10580,.T.);
#14435=ORIENTED_EDGE('',*,*,#10601,.T.);
#14436=ORIENTED_EDGE('',*,*,#10602,.T.);
#14437=ORIENTED_EDGE('',*,*,#10603,.T.);
#14438=ORIENTED_EDGE('',*,*,#10602,.F.);
#14439=ORIENTED_EDGE('',*,*,#10604,.F.);
#14440=ORIENTED_EDGE('',*,*,#10605,.T.);
#14441=ORIENTED_EDGE('',*,*,#10606,.T.);
#14442=ORIENTED_EDGE('',*,*,#10605,.F.);
#14443=ORIENTED_EDGE('',*,*,#10606,.F.);
#14444=ORIENTED_EDGE('',*,*,#10607,.T.);
#14445=ORIENTED_EDGE('',*,*,#10608,.T.);
#14446=ORIENTED_EDGE('',*,*,#10607,.F.);
#14447=ORIENTED_EDGE('',*,*,#10608,.F.);
#14448=ORIENTED_EDGE('',*,*,#10609,.T.);
#14449=ORIENTED_EDGE('',*,*,#10610,.T.);
#14450=ORIENTED_EDGE('',*,*,#10609,.F.);
#14451=ORIENTED_EDGE('',*,*,#10611,.T.);
#14452=ORIENTED_EDGE('',*,*,#10612,.T.);
#14453=ORIENTED_EDGE('',*,*,#10613,.F.);
#14454=ORIENTED_EDGE('',*,*,#10612,.F.);
#14455=ORIENTED_EDGE('',*,*,#10614,.T.);
#14456=ORIENTED_EDGE('',*,*,#10611,.F.);
#14457=ORIENTED_EDGE('',*,*,#10615,.T.);
#14458=ORIENTED_EDGE('',*,*,#10604,.T.);
#14459=ORIENTED_EDGE('',*,*,#10615,.F.);
#14460=ORIENTED_EDGE('',*,*,#10614,.F.);
#14461=ORIENTED_EDGE('',*,*,#10616,.F.);
#14462=ORIENTED_EDGE('',*,*,#10617,.T.);
#14463=ORIENTED_EDGE('',*,*,#10601,.F.);
#14464=ORIENTED_EDGE('',*,*,#10617,.F.);
#14465=ORIENTED_EDGE('',*,*,#10603,.F.);
#14466=ORIENTED_EDGE('',*,*,#10618,.T.);
#14467=ORIENTED_EDGE('',*,*,#10619,.T.);
#14468=ORIENTED_EDGE('',*,*,#10618,.F.);
#14469=ORIENTED_EDGE('',*,*,#10613,.T.);
#14470=ORIENTED_EDGE('',*,*,#10619,.F.);
#14471=ORIENTED_EDGE('',*,*,#10610,.F.);
#14472=ORIENTED_EDGE('',*,*,#10616,.T.);
#14473=ORIENTED_EDGE('',*,*,#10620,.T.);
#14474=ORIENTED_EDGE('',*,*,#10620,.F.);
#14475=ORIENTED_EDGE('',*,*,#10621,.T.);
#14476=ORIENTED_EDGE('',*,*,#10621,.F.);
#14477=ORIENTED_EDGE('',*,*,#10622,.T.);
#14478=ORIENTED_EDGE('',*,*,#10622,.F.);
#14479=ORIENTED_EDGE('',*,*,#10623,.T.);
#14480=ORIENTED_EDGE('',*,*,#10623,.F.);
#14481=ORIENTED_EDGE('',*,*,#10624,.T.);
#14482=ORIENTED_EDGE('',*,*,#10624,.F.);
#14483=ORIENTED_EDGE('',*,*,#10625,.T.);
#14484=ORIENTED_EDGE('',*,*,#10625,.F.);
#14485=ORIENTED_EDGE('',*,*,#10626,.T.);
#14486=ORIENTED_EDGE('',*,*,#10626,.F.);
#14487=ORIENTED_EDGE('',*,*,#10627,.F.);
#14488=ORIENTED_EDGE('',*,*,#10628,.F.);
#14489=ORIENTED_EDGE('',*,*,#10629,.T.);
#14490=ORIENTED_EDGE('',*,*,#10630,.F.);
#14491=ORIENTED_EDGE('',*,*,#10631,.F.);
#14492=ORIENTED_EDGE('',*,*,#10629,.F.);
#14493=ORIENTED_EDGE('',*,*,#10632,.F.);
#14494=ORIENTED_EDGE('',*,*,#10633,.T.);
#14495=ORIENTED_EDGE('',*,*,#10634,.T.);
#14496=ORIENTED_EDGE('',*,*,#10633,.F.);
#14497=ORIENTED_EDGE('',*,*,#10635,.F.);
#14498=ORIENTED_EDGE('',*,*,#10636,.T.);
#14499=ORIENTED_EDGE('',*,*,#10632,.T.);
#14500=ORIENTED_EDGE('',*,*,#10636,.F.);
#14501=ORIENTED_EDGE('',*,*,#10637,.F.);
#14502=ORIENTED_EDGE('',*,*,#10638,.T.);
#14503=ORIENTED_EDGE('',*,*,#10639,.T.);
#14504=ORIENTED_EDGE('',*,*,#10638,.F.);
#14505=ORIENTED_EDGE('',*,*,#10640,.F.);
#14506=ORIENTED_EDGE('',*,*,#10641,.T.);
#14507=ORIENTED_EDGE('',*,*,#10637,.T.);
#14508=ORIENTED_EDGE('',*,*,#10641,.F.);
#14509=ORIENTED_EDGE('',*,*,#10642,.F.);
#14510=ORIENTED_EDGE('',*,*,#10643,.F.);
#14511=ORIENTED_EDGE('',*,*,#10644,.F.);
#14512=ORIENTED_EDGE('',*,*,#10645,.F.);
#14513=ORIENTED_EDGE('',*,*,#10646,.F.);
#14514=ORIENTED_EDGE('',*,*,#10647,.F.);
#14515=ORIENTED_EDGE('',*,*,#10648,.F.);
#14516=ORIENTED_EDGE('',*,*,#10649,.F.);
#14517=ORIENTED_EDGE('',*,*,#10650,.F.);
#14518=ORIENTED_EDGE('',*,*,#10651,.T.);
#14519=ORIENTED_EDGE('',*,*,#10640,.T.);
#14520=ORIENTED_EDGE('',*,*,#10651,.F.);
#14521=ORIENTED_EDGE('',*,*,#10652,.F.);
#14522=ORIENTED_EDGE('',*,*,#10653,.F.);
#14523=ORIENTED_EDGE('',*,*,#10654,.F.);
#14524=ORIENTED_EDGE('',*,*,#10655,.F.);
#14525=ORIENTED_EDGE('',*,*,#10656,.F.);
#14526=ORIENTED_EDGE('',*,*,#10657,.F.);
#14527=ORIENTED_EDGE('',*,*,#10658,.F.);
#14528=ORIENTED_EDGE('',*,*,#10659,.F.);
#14529=ORIENTED_EDGE('',*,*,#10660,.F.);
#14530=ORIENTED_EDGE('',*,*,#10661,.T.);
#14531=ORIENTED_EDGE('',*,*,#10662,.T.);
#14532=ORIENTED_EDGE('',*,*,#10661,.F.);
#14533=ORIENTED_EDGE('',*,*,#10662,.F.);
#14534=ORIENTED_EDGE('',*,*,#10663,.T.);
#14535=ORIENTED_EDGE('',*,*,#10630,.T.);
#14536=ORIENTED_EDGE('',*,*,#10631,.T.);
#14537=ORIENTED_EDGE('',*,*,#10663,.F.);
#14538=ORIENTED_EDGE('',*,*,#10627,.T.);
#14539=ORIENTED_EDGE('',*,*,#10628,.T.);
#14540=ORIENTED_EDGE('',*,*,#10664,.T.);
#14541=ORIENTED_EDGE('',*,*,#10665,.F.);
#14542=ORIENTED_EDGE('',*,*,#10666,.T.);
#14543=ORIENTED_EDGE('',*,*,#10667,.T.);
#14544=ORIENTED_EDGE('',*,*,#10668,.T.);
#14545=ORIENTED_EDGE('',*,*,#10669,.F.);
#14546=ORIENTED_EDGE('',*,*,#10670,.T.);
#14547=ORIENTED_EDGE('',*,*,#10671,.T.);
#14548=ORIENTED_EDGE('',*,*,#10672,.T.);
#14549=ORIENTED_EDGE('',*,*,#10673,.F.);
#14550=ORIENTED_EDGE('',*,*,#10674,.T.);
#14551=ORIENTED_EDGE('',*,*,#10675,.T.);
#14552=ORIENTED_EDGE('',*,*,#10676,.T.);
#14553=ORIENTED_EDGE('',*,*,#10677,.F.);
#14554=ORIENTED_EDGE('',*,*,#10678,.T.);
#14555=ORIENTED_EDGE('',*,*,#10679,.T.);
#14556=ORIENTED_EDGE('',*,*,#10680,.T.);
#14557=ORIENTED_EDGE('',*,*,#10681,.F.);
#14558=ORIENTED_EDGE('',*,*,#10682,.T.);
#14559=ORIENTED_EDGE('',*,*,#10683,.T.);
#14560=ORIENTED_EDGE('',*,*,#10684,.T.);
#14561=ORIENTED_EDGE('',*,*,#10685,.F.);
#14562=ORIENTED_EDGE('',*,*,#10686,.T.);
#14563=ORIENTED_EDGE('',*,*,#10687,.T.);
#14564=ORIENTED_EDGE('',*,*,#10688,.T.);
#14565=ORIENTED_EDGE('',*,*,#10689,.F.);
#14566=ORIENTED_EDGE('',*,*,#10690,.T.);
#14567=ORIENTED_EDGE('',*,*,#10691,.T.);
#14568=ORIENTED_EDGE('',*,*,#10692,.T.);
#14569=ORIENTED_EDGE('',*,*,#10693,.F.);
#14570=ORIENTED_EDGE('',*,*,#10694,.T.);
#14571=ORIENTED_EDGE('',*,*,#10695,.T.);
#14572=ORIENTED_EDGE('',*,*,#10696,.T.);
#14573=ORIENTED_EDGE('',*,*,#10697,.F.);
#14574=ORIENTED_EDGE('',*,*,#10664,.F.);
#14575=ORIENTED_EDGE('',*,*,#10667,.F.);
#14576=ORIENTED_EDGE('',*,*,#10698,.T.);
#14577=ORIENTED_EDGE('',*,*,#10699,.T.);
#14578=ORIENTED_EDGE('',*,*,#10700,.T.);
#14579=ORIENTED_EDGE('',*,*,#10701,.T.);
#14580=ORIENTED_EDGE('',*,*,#10702,.T.);
#14581=ORIENTED_EDGE('',*,*,#10695,.F.);
#14582=ORIENTED_EDGE('',*,*,#10703,.T.);
#14583=ORIENTED_EDGE('',*,*,#10671,.F.);
#14584=ORIENTED_EDGE('',*,*,#10704,.T.);
#14585=ORIENTED_EDGE('',*,*,#10705,.T.);
#14586=ORIENTED_EDGE('',*,*,#10706,.T.);
#14587=ORIENTED_EDGE('',*,*,#10675,.F.);
#14588=ORIENTED_EDGE('',*,*,#10707,.T.);
#14589=ORIENTED_EDGE('',*,*,#10708,.T.);
#14590=ORIENTED_EDGE('',*,*,#10709,.T.);
#14591=ORIENTED_EDGE('',*,*,#10679,.F.);
#14592=ORIENTED_EDGE('',*,*,#10710,.T.);
#14593=ORIENTED_EDGE('',*,*,#10711,.T.);
#14594=ORIENTED_EDGE('',*,*,#10712,.T.);
#14595=ORIENTED_EDGE('',*,*,#10683,.F.);
#14596=ORIENTED_EDGE('',*,*,#10713,.T.);
#14597=ORIENTED_EDGE('',*,*,#10714,.T.);
#14598=ORIENTED_EDGE('',*,*,#10715,.T.);
#14599=ORIENTED_EDGE('',*,*,#10687,.F.);
#14600=ORIENTED_EDGE('',*,*,#10716,.T.);
#14601=ORIENTED_EDGE('',*,*,#10717,.T.);
#14602=ORIENTED_EDGE('',*,*,#10718,.T.);
#14603=ORIENTED_EDGE('',*,*,#10719,.T.);
#14604=ORIENTED_EDGE('',*,*,#10720,.T.);
#14605=ORIENTED_EDGE('',*,*,#10691,.F.);
#14606=ORIENTED_EDGE('',*,*,#10721,.T.);
#14607=ORIENTED_EDGE('',*,*,#10699,.F.);
#14608=ORIENTED_EDGE('',*,*,#10722,.T.);
#14609=ORIENTED_EDGE('',*,*,#10723,.T.);
#14610=ORIENTED_EDGE('',*,*,#10724,.T.);
#14611=ORIENTED_EDGE('',*,*,#10725,.T.);
#14612=ORIENTED_EDGE('',*,*,#10726,.T.);
#14613=ORIENTED_EDGE('',*,*,#10701,.F.);
#14614=ORIENTED_EDGE('',*,*,#10727,.T.);
#14615=ORIENTED_EDGE('',*,*,#10705,.F.);
#14616=ORIENTED_EDGE('',*,*,#10728,.T.);
#14617=ORIENTED_EDGE('',*,*,#10729,.T.);
#14618=ORIENTED_EDGE('',*,*,#10730,.T.);
#14619=ORIENTED_EDGE('',*,*,#10708,.F.);
#14620=ORIENTED_EDGE('',*,*,#10731,.T.);
#14621=ORIENTED_EDGE('',*,*,#10732,.T.);
#14622=ORIENTED_EDGE('',*,*,#10733,.T.);
#14623=ORIENTED_EDGE('',*,*,#10711,.F.);
#14624=ORIENTED_EDGE('',*,*,#10734,.T.);
#14625=ORIENTED_EDGE('',*,*,#10735,.T.);
#14626=ORIENTED_EDGE('',*,*,#10736,.T.);
#14627=ORIENTED_EDGE('',*,*,#10714,.F.);
#14628=ORIENTED_EDGE('',*,*,#10737,.T.);
#14629=ORIENTED_EDGE('',*,*,#10738,.T.);
#14630=ORIENTED_EDGE('',*,*,#10739,.T.);
#14631=ORIENTED_EDGE('',*,*,#10717,.F.);
#14632=ORIENTED_EDGE('',*,*,#10740,.T.);
#14633=ORIENTED_EDGE('',*,*,#10741,.T.);
#14634=ORIENTED_EDGE('',*,*,#10742,.T.);
#14635=ORIENTED_EDGE('',*,*,#10743,.T.);
#14636=ORIENTED_EDGE('',*,*,#10744,.T.);
#14637=ORIENTED_EDGE('',*,*,#10719,.F.);
#14638=ORIENTED_EDGE('',*,*,#10745,.T.);
#14639=ORIENTED_EDGE('',*,*,#10723,.F.);
#14640=ORIENTED_EDGE('',*,*,#10746,.T.);
#14641=ORIENTED_EDGE('',*,*,#10649,.T.);
#14642=ORIENTED_EDGE('',*,*,#10747,.T.);
#14643=ORIENTED_EDGE('',*,*,#10653,.T.);
#14644=ORIENTED_EDGE('',*,*,#10748,.T.);
#14645=ORIENTED_EDGE('',*,*,#10725,.F.);
#14646=ORIENTED_EDGE('',*,*,#10749,.T.);
#14647=ORIENTED_EDGE('',*,*,#10729,.F.);
#14648=ORIENTED_EDGE('',*,*,#10750,.T.);
#14649=ORIENTED_EDGE('',*,*,#10647,.T.);
#14650=ORIENTED_EDGE('',*,*,#10751,.T.);
#14651=ORIENTED_EDGE('',*,*,#10732,.F.);
#14652=ORIENTED_EDGE('',*,*,#10752,.T.);
#14653=ORIENTED_EDGE('',*,*,#10645,.T.);
#14654=ORIENTED_EDGE('',*,*,#10753,.T.);
#14655=ORIENTED_EDGE('',*,*,#10735,.F.);
#14656=ORIENTED_EDGE('',*,*,#10754,.T.);
#14657=ORIENTED_EDGE('',*,*,#10643,.T.);
#14658=ORIENTED_EDGE('',*,*,#10755,.T.);
#14659=ORIENTED_EDGE('',*,*,#10738,.F.);
#14660=ORIENTED_EDGE('',*,*,#10756,.T.);
#14661=ORIENTED_EDGE('',*,*,#10659,.T.);
#14662=ORIENTED_EDGE('',*,*,#10757,.T.);
#14663=ORIENTED_EDGE('',*,*,#10741,.F.);
#14664=ORIENTED_EDGE('',*,*,#10758,.T.);
#14665=ORIENTED_EDGE('',*,*,#10657,.T.);
#14666=ORIENTED_EDGE('',*,*,#10759,.T.);
#14667=ORIENTED_EDGE('',*,*,#10655,.T.);
#14668=ORIENTED_EDGE('',*,*,#10760,.T.);
#14669=ORIENTED_EDGE('',*,*,#10743,.F.);
#14670=ORIENTED_EDGE('',*,*,#10761,.T.);
#14671=ORIENTED_EDGE('',*,*,#10639,.F.);
#14672=ORIENTED_EDGE('',*,*,#10635,.T.);
#14673=ORIENTED_EDGE('',*,*,#10660,.T.);
#14674=ORIENTED_EDGE('',*,*,#10634,.F.);
#14675=ORIENTED_EDGE('',*,*,#10762,.F.);
#14676=ORIENTED_EDGE('',*,*,#10761,.F.);
#14677=ORIENTED_EDGE('',*,*,#10745,.F.);
#14678=ORIENTED_EDGE('',*,*,#10721,.F.);
#14679=ORIENTED_EDGE('',*,*,#10690,.F.);
#14680=ORIENTED_EDGE('',*,*,#10718,.F.);
#14681=ORIENTED_EDGE('',*,*,#10742,.F.);
#14682=ORIENTED_EDGE('',*,*,#10759,.F.);
#14683=ORIENTED_EDGE('',*,*,#10763,.F.);
#14684=ORIENTED_EDGE('',*,*,#10688,.F.);
#14685=ORIENTED_EDGE('',*,*,#10689,.T.);
#14686=ORIENTED_EDGE('',*,*,#10763,.T.);
#14687=ORIENTED_EDGE('',*,*,#10656,.T.);
#14688=ORIENTED_EDGE('',*,*,#10762,.T.);
#14689=ORIENTED_EDGE('',*,*,#10764,.F.);
#14690=ORIENTED_EDGE('',*,*,#10749,.F.);
#14691=ORIENTED_EDGE('',*,*,#10727,.F.);
#14692=ORIENTED_EDGE('',*,*,#10703,.F.);
#14693=ORIENTED_EDGE('',*,*,#10694,.F.);
#14694=ORIENTED_EDGE('',*,*,#10720,.F.);
#14695=ORIENTED_EDGE('',*,*,#10744,.F.);
#14696=ORIENTED_EDGE('',*,*,#10760,.F.);
#14697=ORIENTED_EDGE('',*,*,#10765,.F.);
#14698=ORIENTED_EDGE('',*,*,#10692,.F.);
#14699=ORIENTED_EDGE('',*,*,#10693,.T.);
#14700=ORIENTED_EDGE('',*,*,#10765,.T.);
#14701=ORIENTED_EDGE('',*,*,#10654,.T.);
#14702=ORIENTED_EDGE('',*,*,#10764,.T.);
#14703=ORIENTED_EDGE('',*,*,#10766,.F.);
#14704=ORIENTED_EDGE('',*,*,#10758,.F.);
#14705=ORIENTED_EDGE('',*,*,#10740,.F.);
#14706=ORIENTED_EDGE('',*,*,#10716,.F.);
#14707=ORIENTED_EDGE('',*,*,#10686,.F.);
#14708=ORIENTED_EDGE('',*,*,#10715,.F.);
#14709=ORIENTED_EDGE('',*,*,#10739,.F.);
#14710=ORIENTED_EDGE('',*,*,#10757,.F.);
#14711=ORIENTED_EDGE('',*,*,#10767,.F.);
#14712=ORIENTED_EDGE('',*,*,#10684,.F.);
#14713=ORIENTED_EDGE('',*,*,#10685,.T.);
#14714=ORIENTED_EDGE('',*,*,#10767,.T.);
#14715=ORIENTED_EDGE('',*,*,#10658,.T.);
#14716=ORIENTED_EDGE('',*,*,#10766,.T.);
#14717=ORIENTED_EDGE('',*,*,#10768,.F.);
#14718=ORIENTED_EDGE('',*,*,#10756,.F.);
#14719=ORIENTED_EDGE('',*,*,#10737,.F.);
#14720=ORIENTED_EDGE('',*,*,#10713,.F.);
#14721=ORIENTED_EDGE('',*,*,#10682,.F.);
#14722=ORIENTED_EDGE('',*,*,#10712,.F.);
#14723=ORIENTED_EDGE('',*,*,#10736,.F.);
#14724=ORIENTED_EDGE('',*,*,#10755,.F.);
#14725=ORIENTED_EDGE('',*,*,#10769,.F.);
#14726=ORIENTED_EDGE('',*,*,#10680,.F.);
#14727=ORIENTED_EDGE('',*,*,#10681,.T.);
#14728=ORIENTED_EDGE('',*,*,#10769,.T.);
#14729=ORIENTED_EDGE('',*,*,#10642,.T.);
#14730=ORIENTED_EDGE('',*,*,#10768,.T.);
#14731=ORIENTED_EDGE('',*,*,#10770,.F.);
#14732=ORIENTED_EDGE('',*,*,#10754,.F.);
#14733=ORIENTED_EDGE('',*,*,#10734,.F.);
#14734=ORIENTED_EDGE('',*,*,#10710,.F.);
#14735=ORIENTED_EDGE('',*,*,#10678,.F.);
#14736=ORIENTED_EDGE('',*,*,#10709,.F.);
#14737=ORIENTED_EDGE('',*,*,#10733,.F.);
#14738=ORIENTED_EDGE('',*,*,#10753,.F.);
#14739=ORIENTED_EDGE('',*,*,#10771,.F.);
#14740=ORIENTED_EDGE('',*,*,#10676,.F.);
#14741=ORIENTED_EDGE('',*,*,#10677,.T.);
#14742=ORIENTED_EDGE('',*,*,#10771,.T.);
#14743=ORIENTED_EDGE('',*,*,#10644,.T.);
#14744=ORIENTED_EDGE('',*,*,#10770,.T.);
#14745=ORIENTED_EDGE('',*,*,#10772,.F.);
#14746=ORIENTED_EDGE('',*,*,#10752,.F.);
#14747=ORIENTED_EDGE('',*,*,#10731,.F.);
#14748=ORIENTED_EDGE('',*,*,#10707,.F.);
#14749=ORIENTED_EDGE('',*,*,#10674,.F.);
#14750=ORIENTED_EDGE('',*,*,#10706,.F.);
#14751=ORIENTED_EDGE('',*,*,#10730,.F.);
#14752=ORIENTED_EDGE('',*,*,#10751,.F.);
#14753=ORIENTED_EDGE('',*,*,#10773,.F.);
#14754=ORIENTED_EDGE('',*,*,#10672,.F.);
#14755=ORIENTED_EDGE('',*,*,#10673,.T.);
#14756=ORIENTED_EDGE('',*,*,#10773,.T.);
#14757=ORIENTED_EDGE('',*,*,#10646,.T.);
#14758=ORIENTED_EDGE('',*,*,#10772,.T.);
#14759=ORIENTED_EDGE('',*,*,#10774,.F.);
#14760=ORIENTED_EDGE('',*,*,#10750,.F.);
#14761=ORIENTED_EDGE('',*,*,#10728,.F.);
#14762=ORIENTED_EDGE('',*,*,#10704,.F.);
#14763=ORIENTED_EDGE('',*,*,#10670,.F.);
#14764=ORIENTED_EDGE('',*,*,#10700,.F.);
#14765=ORIENTED_EDGE('',*,*,#10724,.F.);
#14766=ORIENTED_EDGE('',*,*,#10747,.F.);
#14767=ORIENTED_EDGE('',*,*,#10775,.F.);
#14768=ORIENTED_EDGE('',*,*,#10668,.F.);
#14769=ORIENTED_EDGE('',*,*,#10669,.T.);
#14770=ORIENTED_EDGE('',*,*,#10775,.T.);
#14771=ORIENTED_EDGE('',*,*,#10648,.T.);
#14772=ORIENTED_EDGE('',*,*,#10774,.T.);
#14773=ORIENTED_EDGE('',*,*,#10776,.F.);
#14774=ORIENTED_EDGE('',*,*,#10746,.F.);
#14775=ORIENTED_EDGE('',*,*,#10722,.F.);
#14776=ORIENTED_EDGE('',*,*,#10698,.F.);
#14777=ORIENTED_EDGE('',*,*,#10666,.F.);
#14778=ORIENTED_EDGE('',*,*,#10702,.F.);
#14779=ORIENTED_EDGE('',*,*,#10726,.F.);
#14780=ORIENTED_EDGE('',*,*,#10748,.F.);
#14781=ORIENTED_EDGE('',*,*,#10777,.F.);
#14782=ORIENTED_EDGE('',*,*,#10696,.F.);
#14783=ORIENTED_EDGE('',*,*,#10665,.T.);
#14784=ORIENTED_EDGE('',*,*,#10697,.T.);
#14785=ORIENTED_EDGE('',*,*,#10777,.T.);
#14786=ORIENTED_EDGE('',*,*,#10652,.T.);
#14787=ORIENTED_EDGE('',*,*,#10650,.T.);
#14788=ORIENTED_EDGE('',*,*,#10776,.T.);
#18679=PLANE('',#20840);
#18680=PLANE('',#20841);
#18681=PLANE('',#20842);
#18682=PLANE('',#20843);
#18683=PLANE('',#20844);
#18684=PLANE('',#20845);
#18685=PLANE('',#20846);
#18686=PLANE('',#20847);
#18687=PLANE('',#20848);
#18688=PLANE('',#20849);
#18689=PLANE('',#20850);
#18690=PLANE('',#20851);
#18691=PLANE('',#20852);
#18692=PLANE('',#20853);
#18693=PLANE('',#20854);
#18694=PLANE('',#20855);
#18695=PLANE('',#20856);
#18696=PLANE('',#20857);
#18697=PLANE('',#20858);
#18698=PLANE('',#20859);
#18699=PLANE('',#20860);
#18700=PLANE('',#20861);
#18701=PLANE('',#20862);
#18702=PLANE('',#20863);
#18703=PLANE('',#20864);
#18704=PLANE('',#20865);
#18705=PLANE('',#20897);
#18706=PLANE('',#20898);
#18707=PLANE('',#20921);
#18708=PLANE('',#20922);
#18709=PLANE('',#21054);
#18710=PLANE('',#21055);
#18711=PLANE('',#21056);
#18712=PLANE('',#21057);
#18713=PLANE('',#21058);
#18714=PLANE('',#21059);
#18715=PLANE('',#21060);
#18716=PLANE('',#21061);
#18717=PLANE('',#21062);
#18718=PLANE('',#21063);
#18719=PLANE('',#21064);
#18720=PLANE('',#21065);
#18721=PLANE('',#21066);
#18722=PLANE('',#21067);
#18723=PLANE('',#21068);
#18724=PLANE('',#21069);
#18725=PLANE('',#21070);
#18726=PLANE('',#21071);
#18727=PLANE('',#21072);
#18728=PLANE('',#21073);
#18729=PLANE('',#21074);
#18730=PLANE('',#21075);
#18731=PLANE('',#21076);
#18732=PLANE('',#21077);
#18733=PLANE('',#21078);
#18734=PLANE('',#21079);
#19316=ADVANCED_FACE('',(#1459),#889,.F.);
#19317=ADVANCED_FACE('',(#1460),#594,.T.);
#19318=ADVANCED_FACE('',(#1461),#595,.T.);
#19319=ADVANCED_FACE('',(#1462),#536,.T.);
#19320=ADVANCED_FACE('',(#1463),#596,.F.);
#19321=ADVANCED_FACE('',(#1464),#537,.F.);
#19322=ADVANCED_FACE('',(#1465),#597,.F.);
#19323=ADVANCED_FACE('',(#1466),#598,.T.);
#19324=ADVANCED_FACE('',(#1467),#538,.T.);
#19325=ADVANCED_FACE('',(#1468),#539,.T.);
#19326=ADVANCED_FACE('',(#1469),#540,.T.);
#19327=ADVANCED_FACE('',(#1470),#541,.T.);
#19328=ADVANCED_FACE('',(#1471),#542,.T.);
#19329=ADVANCED_FACE('',(#1472),#543,.T.);
#19330=ADVANCED_FACE('',(#1473),#544,.T.);
#19331=ADVANCED_FACE('',(#1474),#545,.T.);
#19332=ADVANCED_FACE('',(#1475),#546,.F.);
#19333=ADVANCED_FACE('',(#1476),#547,.F.);
#19334=ADVANCED_FACE('',(#1477),#548,.F.);
#19335=ADVANCED_FACE('',(#1478),#549,.F.);
#19336=ADVANCED_FACE('',(#1479),#550,.F.);
#19337=ADVANCED_FACE('',(#1480),#551,.F.);
#19338=ADVANCED_FACE('',(#1481),#552,.F.);
#19339=ADVANCED_FACE('',(#1482),#553,.F.);
#19340=ADVANCED_FACE('',(#1483),#554,.F.);
#19341=ADVANCED_FACE('',(#1484),#555,.F.);
#19342=ADVANCED_FACE('',(#1485),#556,.F.);
#19343=ADVANCED_FACE('',(#1486),#557,.F.);
#19344=ADVANCED_FACE('',(#1487),#558,.F.);
#19345=ADVANCED_FACE('',(#1488),#559,.F.);
#19346=ADVANCED_FACE('',(#1489),#560,.F.);
#19347=ADVANCED_FACE('',(#1490),#561,.F.);
#19348=ADVANCED_FACE('',(#1491,#651),#18679,.T.);
#19349=ADVANCED_FACE('',(#1492,#652),#18680,.T.);
#19350=ADVANCED_FACE('',(#1493),#18681,.T.);
#19351=ADVANCED_FACE('',(#1494),#18682,.T.);
#19352=ADVANCED_FACE('',(#1495),#18683,.F.);
#19353=ADVANCED_FACE('',(#1496),#18684,.T.);
#19354=ADVANCED_FACE('',(#1497),#18685,.T.);
#19355=ADVANCED_FACE('',(#1498),#18686,.F.);
#19356=ADVANCED_FACE('',(#1499),#18687,.T.);
#19357=ADVANCED_FACE('',(#1500),#18688,.T.);
#19358=ADVANCED_FACE('',(#1501),#18689,.F.);
#19359=ADVANCED_FACE('',(#1502),#18690,.T.);
#19360=ADVANCED_FACE('',(#1503),#18691,.T.);
#19361=ADVANCED_FACE('',(#1504),#18692,.F.);
#19362=ADVANCED_FACE('',(#1505),#18693,.T.);
#19363=ADVANCED_FACE('',(#1506),#18694,.T.);
#19364=ADVANCED_FACE('',(#1507),#18695,.F.);
#19365=ADVANCED_FACE('',(#1508),#18696,.T.);
#19366=ADVANCED_FACE('',(#1509),#18697,.T.);
#19367=ADVANCED_FACE('',(#1510),#18698,.F.);
#19368=ADVANCED_FACE('',(#1511),#18699,.T.);
#19369=ADVANCED_FACE('',(#1512),#18700,.T.);
#19370=ADVANCED_FACE('',(#1513),#18701,.F.);
#19371=ADVANCED_FACE('',(#1514),#18702,.T.);
#19372=ADVANCED_FACE('',(#1515),#18703,.T.);
#19373=ADVANCED_FACE('',(#1516),#18704,.F.);
#19374=ADVANCED_FACE('',(#1517),#528,.T.);
#19375=ADVANCED_FACE('',(#1518),#599,.F.);
#19376=ADVANCED_FACE('',(#1519),#600,.T.);
#19377=ADVANCED_FACE('',(#1520),#562,.F.);
#19378=ADVANCED_FACE('',(#1521),#890,.F.);
#19379=ADVANCED_FACE('',(#1522),#563,.F.);
#19380=ADVANCED_FACE('',(#1523),#601,.T.);
#19381=ADVANCED_FACE('',(#1524),#602,.T.);
#19382=ADVANCED_FACE('',(#1525),#603,.T.);
#19383=ADVANCED_FACE('',(#1526),#891,.T.);
#19384=ADVANCED_FACE('',(#1527),#892,.T.);
#19385=ADVANCED_FACE('',(#1528,#653),#18705,.F.);
#19386=ADVANCED_FACE('',(#1529,#654),#18706,.F.);
#19387=ADVANCED_FACE('',(#1530),#604,.F.);
#19388=ADVANCED_FACE('',(#1531),#893,.T.);
#19389=ADVANCED_FACE('',(#1532),#605,.T.);
#19390=ADVANCED_FACE('',(#1533),#564,.T.);
#19391=ADVANCED_FACE('',(#1534),#565,.T.);
#19392=ADVANCED_FACE('',(#1535),#606,.T.);
#19393=ADVANCED_FACE('',(#1536),#894,.F.);
#19394=ADVANCED_FACE('',(#1537),#895,.F.);
#19395=ADVANCED_FACE('',(#1538,#655),#18707,.F.);
#19396=ADVANCED_FACE('',(#1539,#656),#18708,.F.);
#19397=ADVANCED_FACE('',(#1540),#529,.T.);
#19398=ADVANCED_FACE('',(#1541),#530,.T.);
#19399=ADVANCED_FACE('',(#1542),#531,.T.);
#19400=ADVANCED_FACE('',(#1543),#532,.T.);
#19401=ADVANCED_FACE('',(#1544),#533,.T.);
#19402=ADVANCED_FACE('',(#1545),#534,.T.);
#19403=ADVANCED_FACE('',(#1546),#535,.T.);
#19404=ADVANCED_FACE('',(#1547),#607,.F.);
#19405=ADVANCED_FACE('',(#1548),#896,.F.);
#19406=ADVANCED_FACE('',(#1549),#608,.T.);
#19407=ADVANCED_FACE('',(#1550),#609,.T.);
#19408=ADVANCED_FACE('',(#1551),#566,.T.);
#19409=ADVANCED_FACE('',(#1552),#610,.F.);
#19410=ADVANCED_FACE('',(#1553),#611,.F.);
#19411=ADVANCED_FACE('',(#1554),#567,.F.);
#19412=ADVANCED_FACE('',(#1555),#612,.T.);
#19413=ADVANCED_FACE('',(#1556),#568,.T.);
#19414=ADVANCED_FACE('',(#1557),#569,.T.);
#19415=ADVANCED_FACE('',(#1558),#570,.T.);
#19416=ADVANCED_FACE('',(#1559),#571,.T.);
#19417=ADVANCED_FACE('',(#1560),#572,.T.);
#19418=ADVANCED_FACE('',(#1561),#573,.T.);
#19419=ADVANCED_FACE('',(#1562),#574,.T.);
#19420=ADVANCED_FACE('',(#1563),#575,.T.);
#19421=ADVANCED_FACE('',(#1564),#576,.F.);
#19422=ADVANCED_FACE('',(#1565),#577,.F.);
#19423=ADVANCED_FACE('',(#1566),#578,.F.);
#19424=ADVANCED_FACE('',(#1567),#579,.F.);
#19425=ADVANCED_FACE('',(#1568),#580,.F.);
#19426=ADVANCED_FACE('',(#1569),#581,.F.);
#19427=ADVANCED_FACE('',(#1570),#582,.F.);
#19428=ADVANCED_FACE('',(#1571),#583,.F.);
#19429=ADVANCED_FACE('',(#1572),#584,.F.);
#19430=ADVANCED_FACE('',(#1573),#585,.F.);
#19431=ADVANCED_FACE('',(#1574),#586,.F.);
#19432=ADVANCED_FACE('',(#1575),#587,.F.);
#19433=ADVANCED_FACE('',(#1576),#588,.F.);
#19434=ADVANCED_FACE('',(#1577),#589,.F.);
#19435=ADVANCED_FACE('',(#1578),#590,.F.);
#19436=ADVANCED_FACE('',(#1579),#591,.F.);
#19437=ADVANCED_FACE('',(#1580,#657),#18709,.T.);
#19438=ADVANCED_FACE('',(#1581,#658),#18710,.T.);
#19439=ADVANCED_FACE('',(#1582),#18711,.T.);
#19440=ADVANCED_FACE('',(#1583),#18712,.T.);
#19441=ADVANCED_FACE('',(#1584),#18713,.F.);
#19442=ADVANCED_FACE('',(#1585),#18714,.T.);
#19443=ADVANCED_FACE('',(#1586),#18715,.T.);
#19444=ADVANCED_FACE('',(#1587),#18716,.F.);
#19445=ADVANCED_FACE('',(#1588),#18717,.T.);
#19446=ADVANCED_FACE('',(#1589),#18718,.T.);
#19447=ADVANCED_FACE('',(#1590),#18719,.F.);
#19448=ADVANCED_FACE('',(#1591),#18720,.T.);
#19449=ADVANCED_FACE('',(#1592),#18721,.T.);
#19450=ADVANCED_FACE('',(#1593),#18722,.F.);
#19451=ADVANCED_FACE('',(#1594),#18723,.T.);
#19452=ADVANCED_FACE('',(#1595),#18724,.T.);
#19453=ADVANCED_FACE('',(#1596),#18725,.F.);
#19454=ADVANCED_FACE('',(#1597),#18726,.T.);
#19455=ADVANCED_FACE('',(#1598),#18727,.T.);
#19456=ADVANCED_FACE('',(#1599),#18728,.F.);
#19457=ADVANCED_FACE('',(#1600),#18729,.T.);
#19458=ADVANCED_FACE('',(#1601),#18730,.T.);
#19459=ADVANCED_FACE('',(#1602),#18731,.F.);
#19460=ADVANCED_FACE('',(#1603),#18732,.T.);
#19461=ADVANCED_FACE('',(#1604),#18733,.T.);
#19462=ADVANCED_FACE('',(#1605),#18734,.F.);
#20114=CLOSED_SHELL('',(#19316,#19317,#19318,#19319,#19320,#19321,#19322,
#19323,#19324,#19325,#19326,#19327,#19328,#19329,#19330,#19331,#19332,#19333,
#19334,#19335,#19336,#19337,#19338,#19339,#19340,#19341,#19342,#19343,#19344,
#19345,#19346,#19347,#19348,#19349,#19350,#19351,#19352,#19353,#19354,#19355,
#19356,#19357,#19358,#19359,#19360,#19361,#19362,#19363,#19364,#19365,#19366,
#19367,#19368,#19369,#19370,#19371,#19372,#19373));
#20115=CLOSED_SHELL('',(#19374));
#20116=CLOSED_SHELL('',(#19375,#19376,#19377,#19378,#19379,#19380,#19381,
#19382,#19383,#19384,#19385,#19386));
#20117=CLOSED_SHELL('',(#19387,#19388,#19389,#19390,#19391,#19392,#19393,
#19394,#19395,#19396));
#20118=CLOSED_SHELL('',(#19397));
#20119=CLOSED_SHELL('',(#19398));
#20120=CLOSED_SHELL('',(#19399));
#20121=CLOSED_SHELL('',(#19400));
#20122=CLOSED_SHELL('',(#19401));
#20123=CLOSED_SHELL('',(#19402));
#20124=CLOSED_SHELL('',(#19403));
#20125=CLOSED_SHELL('',(#19404,#19405,#19406,#19407,#19408,#19409,#19410,
#19411,#19412,#19413,#19414,#19415,#19416,#19417,#19418,#19419,#19420,#19421,
#19422,#19423,#19424,#19425,#19426,#19427,#19428,#19429,#19430,#19431,#19432,
#19433,#19434,#19435,#19436,#19437,#19438,#19439,#19440,#19441,#19442,#19443,
#19444,#19445,#19446,#19447,#19448,#19449,#19450,#19451,#19452,#19453,#19454,
#19455,#19456,#19457,#19458,#19459,#19460,#19461,#19462));
#20727=AXIS2_PLACEMENT_3D('',#28602,#23372,#23373);
#20728=AXIS2_PLACEMENT_3D('',#28603,#23374,#23375);
#20729=AXIS2_PLACEMENT_3D('',#28605,#23376,#23377);
#20730=AXIS2_PLACEMENT_3D('',#28608,#23379,#23380);
#20731=AXIS2_PLACEMENT_3D('',#28609,#23381,#23382);
#20732=AXIS2_PLACEMENT_3D('',#28611,#23383,#23384);
#20733=AXIS2_PLACEMENT_3D('',#28612,#23385,#23386);
#20734=AXIS2_PLACEMENT_3D('',#28613,#23387,#23388);
#20735=AXIS2_PLACEMENT_3D('',#28615,#23389,#23390);
#20736=AXIS2_PLACEMENT_3D('',#28617,#23391,#23392);
#20737=AXIS2_PLACEMENT_3D('',#28618,#23393,#23394);
#20738=AXIS2_PLACEMENT_3D('',#28619,#23395,#23396);
#20739=AXIS2_PLACEMENT_3D('',#28621,#23397,#23398);
#20740=AXIS2_PLACEMENT_3D('',#28623,#23400,#23401);
#20741=AXIS2_PLACEMENT_3D('',#28626,#23402,#23403);
#20742=AXIS2_PLACEMENT_3D('',#28628,#23404,#23405);
#20743=AXIS2_PLACEMENT_3D('',#28630,#23406,#23407);
#20744=AXIS2_PLACEMENT_3D('',#28632,#23408,#23409);
#20745=AXIS2_PLACEMENT_3D('',#28634,#23410,#23411);
#20746=AXIS2_PLACEMENT_3D('',#28636,#23412,#23413);
#20747=AXIS2_PLACEMENT_3D('',#28638,#23414,#23415);
#20748=AXIS2_PLACEMENT_3D('',#28640,#23416,#23417);
#20749=AXIS2_PLACEMENT_3D('',#28642,#23418,#23419);
#20750=AXIS2_PLACEMENT_3D('',#28643,#23420,#23421);
#20751=AXIS2_PLACEMENT_3D('',#28645,#23422,#23423);
#20752=AXIS2_PLACEMENT_3D('',#28647,#23424,#23425);
#20753=AXIS2_PLACEMENT_3D('',#28649,#23426,#23427);
#20754=AXIS2_PLACEMENT_3D('',#28651,#23428,#23429);
#20755=AXIS2_PLACEMENT_3D('',#28653,#23430,#23431);
#20756=AXIS2_PLACEMENT_3D('',#28655,#23432,#23433);
#20757=AXIS2_PLACEMENT_3D('',#28657,#23434,#23435);
#20758=AXIS2_PLACEMENT_3D('',#28658,#23436,#23437);
#20759=AXIS2_PLACEMENT_3D('',#28659,#23438,#23439);
#20760=AXIS2_PLACEMENT_3D('',#28661,#23440,#23441);
#20761=AXIS2_PLACEMENT_3D('',#28664,#23443,#23444);
#20762=AXIS2_PLACEMENT_3D('',#28665,#23445,#23446);
#20763=AXIS2_PLACEMENT_3D('',#28667,#23447,#23448);
#20764=AXIS2_PLACEMENT_3D('',#28668,#23449,#23450);
#20765=AXIS2_PLACEMENT_3D('',#28669,#23451,#23452);
#20766=AXIS2_PLACEMENT_3D('',#28671,#23453,#23454);
#20767=AXIS2_PLACEMENT_3D('',#28673,#23455,#23456);
#20768=AXIS2_PLACEMENT_3D('',#28675,#23457,#23458);
#20769=AXIS2_PLACEMENT_3D('',#28677,#23459,#23460);
#20770=AXIS2_PLACEMENT_3D('',#28679,#23461,#23462);
#20771=AXIS2_PLACEMENT_3D('',#28681,#23463,#23464);
#20772=AXIS2_PLACEMENT_3D('',#28683,#23465,#23466);
#20773=AXIS2_PLACEMENT_3D('',#28685,#23467,#23468);
#20774=AXIS2_PLACEMENT_3D('',#28687,#23469,#23470);
#20775=AXIS2_PLACEMENT_3D('',#28689,#23471,#23472);
#20776=AXIS2_PLACEMENT_3D('',#28691,#23473,#23474);
#20777=AXIS2_PLACEMENT_3D('',#28693,#23475,#23476);
#20778=AXIS2_PLACEMENT_3D('',#28695,#23477,#23478);
#20779=AXIS2_PLACEMENT_3D('',#28697,#23479,#23480);
#20780=AXIS2_PLACEMENT_3D('',#28699,#23481,#23482);
#20781=AXIS2_PLACEMENT_3D('',#28701,#23483,#23484);
#20782=AXIS2_PLACEMENT_3D('',#28703,#23485,#23486);
#20783=AXIS2_PLACEMENT_3D('',#28705,#23487,#23488);
#20784=AXIS2_PLACEMENT_3D('',#28707,#23489,#23490);
#20785=AXIS2_PLACEMENT_3D('',#28709,#23491,#23492);
#20786=AXIS2_PLACEMENT_3D('',#28711,#23493,#23494);
#20787=AXIS2_PLACEMENT_3D('',#28713,#23495,#23496);
#20788=AXIS2_PLACEMENT_3D('',#28715,#23497,#23498);
#20789=AXIS2_PLACEMENT_3D('',#28717,#23499,#23500);
#20790=AXIS2_PLACEMENT_3D('',#28719,#23501,#23502);
#20791=AXIS2_PLACEMENT_3D('',#28721,#23503,#23504);
#20792=AXIS2_PLACEMENT_3D('',#28723,#23505,#23506);
#20793=AXIS2_PLACEMENT_3D('',#28725,#23507,#23508);
#20794=AXIS2_PLACEMENT_3D('',#28727,#23509,#23510);
#20795=AXIS2_PLACEMENT_3D('',#28729,#23511,#23512);
#20796=AXIS2_PLACEMENT_3D('',#28731,#23513,#23514);
#20797=AXIS2_PLACEMENT_3D('',#28733,#23515,#23516);
#20798=AXIS2_PLACEMENT_3D('',#28735,#23517,#23518);
#20799=AXIS2_PLACEMENT_3D('',#28736,#23519,#23520);
#20800=AXIS2_PLACEMENT_3D('',#28737,#23521,#23522);
#20801=AXIS2_PLACEMENT_3D('',#28741,#23524,#23525);
#20802=AXIS2_PLACEMENT_3D('',#28743,#23527,#23528);
#20803=AXIS2_PLACEMENT_3D('',#28746,#23529,#23530);
#20804=AXIS2_PLACEMENT_3D('',#28749,#23533,#23534);
#20805=AXIS2_PLACEMENT_3D('',#28753,#23536,#23537);
#20806=AXIS2_PLACEMENT_3D('',#28755,#23539,#23540);
#20807=AXIS2_PLACEMENT_3D('',#28759,#23542,#23543);
#20808=AXIS2_PLACEMENT_3D('',#28761,#23545,#23546);
#20809=AXIS2_PLACEMENT_3D('',#28765,#23548,#23549);
#20810=AXIS2_PLACEMENT_3D('',#28767,#23551,#23552);
#20811=AXIS2_PLACEMENT_3D('',#28771,#23554,#23555);
#20812=AXIS2_PLACEMENT_3D('',#28773,#23557,#23558);
#20813=AXIS2_PLACEMENT_3D('',#28777,#23560,#23561);
#20814=AXIS2_PLACEMENT_3D('',#28779,#23563,#23564);
#20815=AXIS2_PLACEMENT_3D('',#28782,#23565,#23566);
#20816=AXIS2_PLACEMENT_3D('',#28785,#23569,#23570);
#20817=AXIS2_PLACEMENT_3D('',#28789,#23572,#23573);
#20818=AXIS2_PLACEMENT_3D('',#28791,#23575,#23576);
#20819=AXIS2_PLACEMENT_3D('',#28794,#23577,#23578);
#20820=AXIS2_PLACEMENT_3D('',#28797,#23581,#23582);
#20821=AXIS2_PLACEMENT_3D('',#28801,#23584,#23585);
#20822=AXIS2_PLACEMENT_3D('',#28803,#23587,#23588);
#20823=AXIS2_PLACEMENT_3D('',#28807,#23590,#23591);
#20824=AXIS2_PLACEMENT_3D('',#28809,#23593,#23594);
#20825=AXIS2_PLACEMENT_3D('',#28813,#23596,#23597);
#20826=AXIS2_PLACEMENT_3D('',#28815,#23599,#23600);
#20827=AXIS2_PLACEMENT_3D('',#28819,#23602,#23603);
#20828=AXIS2_PLACEMENT_3D('',#28821,#23605,#23606);
#20829=AXIS2_PLACEMENT_3D('',#28825,#23608,#23609);
#20830=AXIS2_PLACEMENT_3D('',#28827,#23611,#23612);
#20831=AXIS2_PLACEMENT_3D('',#28830,#23613,#23614);
#20832=AXIS2_PLACEMENT_3D('',#28833,#23617,#23618);
#20833=AXIS2_PLACEMENT_3D('',#28836,#23621,#23622);
#20834=AXIS2_PLACEMENT_3D('',#28839,#23625,#23626);
#20835=AXIS2_PLACEMENT_3D('',#28842,#23629,#23630);
#20836=AXIS2_PLACEMENT_3D('',#28845,#23633,#23634);
#20837=AXIS2_PLACEMENT_3D('',#28848,#23637,#23638);
#20838=AXIS2_PLACEMENT_3D('',#28851,#23641,#23642);
#20839=AXIS2_PLACEMENT_3D('',#28854,#23645,#23646);
#20840=AXIS2_PLACEMENT_3D('',#28857,#23649,#23650);
#20841=AXIS2_PLACEMENT_3D('',#28858,#23651,#23652);
#20842=AXIS2_PLACEMENT_3D('',#28859,#23653,#23654);
#20843=AXIS2_PLACEMENT_3D('',#28861,#23656,#23657);
#20844=AXIS2_PLACEMENT_3D('',#28863,#23659,#23660);
#20845=AXIS2_PLACEMENT_3D('',#28864,#23661,#23662);
#20846=AXIS2_PLACEMENT_3D('',#28866,#23664,#23665);
#20847=AXIS2_PLACEMENT_3D('',#28868,#23667,#23668);
#20848=AXIS2_PLACEMENT_3D('',#28869,#23669,#23670);
#20849=AXIS2_PLACEMENT_3D('',#28871,#23672,#23673);
#20850=AXIS2_PLACEMENT_3D('',#28873,#23675,#23676);
#20851=AXIS2_PLACEMENT_3D('',#28874,#23677,#23678);
#20852=AXIS2_PLACEMENT_3D('',#28876,#23680,#23681);
#20853=AXIS2_PLACEMENT_3D('',#28878,#23683,#23684);
#20854=AXIS2_PLACEMENT_3D('',#28879,#23685,#23686);
#20855=AXIS2_PLACEMENT_3D('',#28881,#23688,#23689);
#20856=AXIS2_PLACEMENT_3D('',#28883,#23691,#23692);
#20857=AXIS2_PLACEMENT_3D('',#28884,#23693,#23694);
#20858=AXIS2_PLACEMENT_3D('',#28886,#23696,#23697);
#20859=AXIS2_PLACEMENT_3D('',#28888,#23699,#23700);
#20860=AXIS2_PLACEMENT_3D('',#28889,#23701,#23702);
#20861=AXIS2_PLACEMENT_3D('',#28891,#23704,#23705);
#20862=AXIS2_PLACEMENT_3D('',#28893,#23707,#23708);
#20863=AXIS2_PLACEMENT_3D('',#28894,#23709,#23710);
#20864=AXIS2_PLACEMENT_3D('',#28896,#23712,#23713);
#20865=AXIS2_PLACEMENT_3D('',#28898,#23715,#23716);
#20866=AXIS2_PLACEMENT_3D('',#28899,#23717,#23718);
#20867=AXIS2_PLACEMENT_3D('',#28902,#23719,#23720);
#20868=AXIS2_PLACEMENT_3D('',#28903,#23721,#23722);
#20869=AXIS2_PLACEMENT_3D('',#28905,#23723,#23724);
#20870=AXIS2_PLACEMENT_3D('',#28907,#23725,#23726);
#20871=AXIS2_PLACEMENT_3D('',#28908,#23727,#23728);
#20872=AXIS2_PLACEMENT_3D('',#28909,#23729,#23730);
#20873=AXIS2_PLACEMENT_3D('',#28911,#23731,#23732);
#20874=AXIS2_PLACEMENT_3D('',#28913,#23733,#23734);
#20875=AXIS2_PLACEMENT_3D('',#28915,#23735,#23736);
#20876=AXIS2_PLACEMENT_3D('',#28916,#23737,#23738);
#20877=AXIS2_PLACEMENT_3D('',#28917,#23739,#23740);
#20878=AXIS2_PLACEMENT_3D('',#28920,#23741,#23742);
#20879=AXIS2_PLACEMENT_3D('',#28922,#23744,#23745);
#20880=AXIS2_PLACEMENT_3D('',#28923,#23746,#23747);
#20881=AXIS2_PLACEMENT_3D('',#28926,#23749,#23750);
#20882=AXIS2_PLACEMENT_3D('',#28927,#23751,#23752);
#20883=AXIS2_PLACEMENT_3D('',#28930,#23754,#23755);
#20884=AXIS2_PLACEMENT_3D('',#28931,#23756,#23757);
#20885=AXIS2_PLACEMENT_3D('',#28933,#23758,#23759);
#20886=AXIS2_PLACEMENT_3D('',#28934,#23760,#23761);
#20887=AXIS2_PLACEMENT_3D('',#28935,#23762,#23763);
#20888=AXIS2_PLACEMENT_3D('',#28937,#23764,#23765);
#20889=AXIS2_PLACEMENT_3D('',#28939,#23766,#23767);
#20890=AXIS2_PLACEMENT_3D('',#28940,#23768,#23769);
#20891=AXIS2_PLACEMENT_3D('',#28941,#23770,#23771);
#20892=AXIS2_PLACEMENT_3D('',#28943,#23772,#23773);
#20893=AXIS2_PLACEMENT_3D('',#28945,#23774,#23775);
#20894=AXIS2_PLACEMENT_3D('',#28946,#23776,#23777);
#20895=AXIS2_PLACEMENT_3D('',#28947,#23778,#23779);
#20896=AXIS2_PLACEMENT_3D('',#28949,#23781,#23782);
#20897=AXIS2_PLACEMENT_3D('',#28951,#23784,#23785);
#20898=AXIS2_PLACEMENT_3D('',#28952,#23786,#23787);
#20899=AXIS2_PLACEMENT_3D('',#28953,#23788,#23789);
#20900=AXIS2_PLACEMENT_3D('',#28955,#23790,#23791);
#20901=AXIS2_PLACEMENT_3D('',#28957,#23792,#23793);
#20902=AXIS2_PLACEMENT_3D('',#28958,#23794,#23795);
#20903=AXIS2_PLACEMENT_3D('',#28959,#23796,#23797);
#20904=AXIS2_PLACEMENT_3D('',#28961,#23798,#23799);
#20905=AXIS2_PLACEMENT_3D('',#28964,#23801,#23802);
#20906=AXIS2_PLACEMENT_3D('',#28965,#23803,#23804);
#20907=AXIS2_PLACEMENT_3D('',#28967,#23805,#23806);
#20908=AXIS2_PLACEMENT_3D('',#28968,#23807,#23808);
#20909=AXIS2_PLACEMENT_3D('',#28969,#23809,#23810);
#20910=AXIS2_PLACEMENT_3D('',#28972,#23812,#23813);
#20911=AXIS2_PLACEMENT_3D('',#28973,#23814,#23815);
#20912=AXIS2_PLACEMENT_3D('',#28976,#23816,#23817);
#20913=AXIS2_PLACEMENT_3D('',#28979,#23819,#23820);
#20914=AXIS2_PLACEMENT_3D('',#28980,#23821,#23822);
#20915=AXIS2_PLACEMENT_3D('',#28981,#23823,#23824);
#20916=AXIS2_PLACEMENT_3D('',#28982,#23825,#23826);
#20917=AXIS2_PLACEMENT_3D('',#28983,#23827,#23828);
#20918=AXIS2_PLACEMENT_3D('',#28985,#23829,#23830);
#20919=AXIS2_PLACEMENT_3D('',#28987,#23832,#23833);
#20920=AXIS2_PLACEMENT_3D('',#28990,#23835,#23836);
#20921=AXIS2_PLACEMENT_3D('',#28991,#23837,#23838);
#20922=AXIS2_PLACEMENT_3D('',#28992,#23839,#23840);
#20923=AXIS2_PLACEMENT_3D('',#28993,#23841,#23842);
#20924=AXIS2_PLACEMENT_3D('',#28996,#23843,#23844);
#20925=AXIS2_PLACEMENT_3D('',#28997,#23845,#23846);
#20926=AXIS2_PLACEMENT_3D('',#29000,#23847,#23848);
#20927=AXIS2_PLACEMENT_3D('',#29001,#23849,#23850);
#20928=AXIS2_PLACEMENT_3D('',#29004,#23851,#23852);
#20929=AXIS2_PLACEMENT_3D('',#29005,#23853,#23854);
#20930=AXIS2_PLACEMENT_3D('',#29008,#23855,#23856);
#20931=AXIS2_PLACEMENT_3D('',#29009,#23857,#23858);
#20932=AXIS2_PLACEMENT_3D('',#29012,#23859,#23860);
#20933=AXIS2_PLACEMENT_3D('',#29013,#23861,#23862);
#20934=AXIS2_PLACEMENT_3D('',#29016,#23863,#23864);
#20935=AXIS2_PLACEMENT_3D('',#29017,#23865,#23866);
#20936=AXIS2_PLACEMENT_3D('',#29020,#23867,#23868);
#20937=AXIS2_PLACEMENT_3D('',#29021,#23869,#23870);
#20938=AXIS2_PLACEMENT_3D('',#29024,#23871,#23872);
#20939=AXIS2_PLACEMENT_3D('',#29025,#23873,#23874);
#20940=AXIS2_PLACEMENT_3D('',#29027,#23875,#23876);
#20941=AXIS2_PLACEMENT_3D('',#29029,#23877,#23878);
#20942=AXIS2_PLACEMENT_3D('',#29030,#23879,#23880);
#20943=AXIS2_PLACEMENT_3D('',#29031,#23881,#23882);
#20944=AXIS2_PLACEMENT_3D('',#29033,#23883,#23884);
#20945=AXIS2_PLACEMENT_3D('',#29036,#23886,#23887);
#20946=AXIS2_PLACEMENT_3D('',#29037,#23888,#23889);
#20947=AXIS2_PLACEMENT_3D('',#29039,#23890,#23891);
#20948=AXIS2_PLACEMENT_3D('',#29040,#23892,#23893);
#20949=AXIS2_PLACEMENT_3D('',#29041,#23894,#23895);
#20950=AXIS2_PLACEMENT_3D('',#29043,#23896,#23897);
#20951=AXIS2_PLACEMENT_3D('',#29045,#23898,#23899);
#20952=AXIS2_PLACEMENT_3D('',#29046,#23900,#23901);
#20953=AXIS2_PLACEMENT_3D('',#29047,#23902,#23903);
#20954=AXIS2_PLACEMENT_3D('',#29049,#23904,#23905);
#20955=AXIS2_PLACEMENT_3D('',#29051,#23907,#23908);
#20956=AXIS2_PLACEMENT_3D('',#29054,#23909,#23910);
#20957=AXIS2_PLACEMENT_3D('',#29056,#23911,#23912);
#20958=AXIS2_PLACEMENT_3D('',#29058,#23913,#23914);
#20959=AXIS2_PLACEMENT_3D('',#29060,#23915,#23916);
#20960=AXIS2_PLACEMENT_3D('',#29062,#23917,#23918);
#20961=AXIS2_PLACEMENT_3D('',#29064,#23919,#23920);
#20962=AXIS2_PLACEMENT_3D('',#29066,#23921,#23922);
#20963=AXIS2_PLACEMENT_3D('',#29068,#23923,#23924);
#20964=AXIS2_PLACEMENT_3D('',#29070,#23925,#23926);
#20965=AXIS2_PLACEMENT_3D('',#29071,#23927,#23928);
#20966=AXIS2_PLACEMENT_3D('',#29073,#23929,#23930);
#20967=AXIS2_PLACEMENT_3D('',#29075,#23931,#23932);
#20968=AXIS2_PLACEMENT_3D('',#29077,#23933,#23934);
#20969=AXIS2_PLACEMENT_3D('',#29079,#23935,#23936);
#20970=AXIS2_PLACEMENT_3D('',#29081,#23937,#23938);
#20971=AXIS2_PLACEMENT_3D('',#29083,#23939,#23940);
#20972=AXIS2_PLACEMENT_3D('',#29085,#23941,#23942);
#20973=AXIS2_PLACEMENT_3D('',#29086,#23943,#23944);
#20974=AXIS2_PLACEMENT_3D('',#29087,#23945,#23946);
#20975=AXIS2_PLACEMENT_3D('',#29089,#23947,#23948);
#20976=AXIS2_PLACEMENT_3D('',#29091,#23949,#23950);
#20977=AXIS2_PLACEMENT_3D('',#29092,#23951,#23952);
#20978=AXIS2_PLACEMENT_3D('',#29093,#23953,#23954);
#20979=AXIS2_PLACEMENT_3D('',#29095,#23956,#23957);
#20980=AXIS2_PLACEMENT_3D('',#29097,#23958,#23959);
#20981=AXIS2_PLACEMENT_3D('',#29099,#23960,#23961);
#20982=AXIS2_PLACEMENT_3D('',#29101,#23962,#23963);
#20983=AXIS2_PLACEMENT_3D('',#29103,#23964,#23965);
#20984=AXIS2_PLACEMENT_3D('',#29105,#23966,#23967);
#20985=AXIS2_PLACEMENT_3D('',#29107,#23968,#23969);
#20986=AXIS2_PLACEMENT_3D('',#29109,#23970,#23971);
#20987=AXIS2_PLACEMENT_3D('',#29111,#23972,#23973);
#20988=AXIS2_PLACEMENT_3D('',#29113,#23974,#23975);
#20989=AXIS2_PLACEMENT_3D('',#29115,#23976,#23977);
#20990=AXIS2_PLACEMENT_3D('',#29117,#23978,#23979);
#20991=AXIS2_PLACEMENT_3D('',#29119,#23980,#23981);
#20992=AXIS2_PLACEMENT_3D('',#29121,#23982,#23983);
#20993=AXIS2_PLACEMENT_3D('',#29123,#23984,#23985);
#20994=AXIS2_PLACEMENT_3D('',#29125,#23986,#23987);
#20995=AXIS2_PLACEMENT_3D('',#29127,#23988,#23989);
#20996=AXIS2_PLACEMENT_3D('',#29129,#23990,#23991);
#20997=AXIS2_PLACEMENT_3D('',#29131,#23992,#23993);
#20998=AXIS2_PLACEMENT_3D('',#29133,#23994,#23995);
#20999=AXIS2_PLACEMENT_3D('',#29135,#23996,#23997);
#21000=AXIS2_PLACEMENT_3D('',#29137,#23998,#23999);
#21001=AXIS2_PLACEMENT_3D('',#29139,#24000,#24001);
#21002=AXIS2_PLACEMENT_3D('',#29141,#24002,#24003);
#21003=AXIS2_PLACEMENT_3D('',#29143,#24004,#24005);
#21004=AXIS2_PLACEMENT_3D('',#29145,#24006,#24007);
#21005=AXIS2_PLACEMENT_3D('',#29147,#24008,#24009);
#21006=AXIS2_PLACEMENT_3D('',#29149,#24010,#24011);
#21007=AXIS2_PLACEMENT_3D('',#29151,#24012,#24013);
#21008=AXIS2_PLACEMENT_3D('',#29153,#24014,#24015);
#21009=AXIS2_PLACEMENT_3D('',#29155,#24016,#24017);
#21010=AXIS2_PLACEMENT_3D('',#29157,#24018,#24019);
#21011=AXIS2_PLACEMENT_3D('',#29159,#24020,#24021);
#21012=AXIS2_PLACEMENT_3D('',#29161,#24022,#24023);
#21013=AXIS2_PLACEMENT_3D('',#29162,#24024,#24025);
#21014=AXIS2_PLACEMENT_3D('',#29163,#24026,#24027);
#21015=AXIS2_PLACEMENT_3D('',#29167,#24029,#24030);
#21016=AXIS2_PLACEMENT_3D('',#29169,#24032,#24033);
#21017=AXIS2_PLACEMENT_3D('',#29172,#24034,#24035);
#21018=AXIS2_PLACEMENT_3D('',#29175,#24038,#24039);
#21019=AXIS2_PLACEMENT_3D('',#29179,#24041,#24042);
#21020=AXIS2_PLACEMENT_3D('',#29181,#24044,#24045);
#21021=AXIS2_PLACEMENT_3D('',#29185,#24047,#24048);
#21022=AXIS2_PLACEMENT_3D('',#29187,#24050,#24051);
#21023=AXIS2_PLACEMENT_3D('',#29191,#24053,#24054);
#21024=AXIS2_PLACEMENT_3D('',#29193,#24056,#24057);
#21025=AXIS2_PLACEMENT_3D('',#29197,#24059,#24060);
#21026=AXIS2_PLACEMENT_3D('',#29199,#24062,#24063);
#21027=AXIS2_PLACEMENT_3D('',#29203,#24065,#24066);
#21028=AXIS2_PLACEMENT_3D('',#29205,#24068,#24069);
#21029=AXIS2_PLACEMENT_3D('',#29208,#24070,#24071);
#21030=AXIS2_PLACEMENT_3D('',#29211,#24074,#24075);
#21031=AXIS2_PLACEMENT_3D('',#29215,#24077,#24078);
#21032=AXIS2_PLACEMENT_3D('',#29217,#24080,#24081);
#21033=AXIS2_PLACEMENT_3D('',#29220,#24082,#24083);
#21034=AXIS2_PLACEMENT_3D('',#29223,#24086,#24087);
#21035=AXIS2_PLACEMENT_3D('',#29227,#24089,#24090);
#21036=AXIS2_PLACEMENT_3D('',#29229,#24092,#24093);
#21037=AXIS2_PLACEMENT_3D('',#29233,#24095,#24096);
#21038=AXIS2_PLACEMENT_3D('',#29235,#24098,#24099);
#21039=AXIS2_PLACEMENT_3D('',#29239,#24101,#24102);
#21040=AXIS2_PLACEMENT_3D('',#29241,#24104,#24105);
#21041=AXIS2_PLACEMENT_3D('',#29245,#24107,#24108);
#21042=AXIS2_PLACEMENT_3D('',#29247,#24110,#24111);
#21043=AXIS2_PLACEMENT_3D('',#29251,#24113,#24114);
#21044=AXIS2_PLACEMENT_3D('',#29253,#24116,#24117);
#21045=AXIS2_PLACEMENT_3D('',#29256,#24118,#24119);
#21046=AXIS2_PLACEMENT_3D('',#29259,#24122,#24123);
#21047=AXIS2_PLACEMENT_3D('',#29262,#24126,#24127);
#21048=AXIS2_PLACEMENT_3D('',#29265,#24130,#24131);
#21049=AXIS2_PLACEMENT_3D('',#29268,#24134,#24135);
#21050=AXIS2_PLACEMENT_3D('',#29271,#24138,#24139);
#21051=AXIS2_PLACEMENT_3D('',#29274,#24142,#24143);
#21052=AXIS2_PLACEMENT_3D('',#29277,#24146,#24147);
#21053=AXIS2_PLACEMENT_3D('',#29280,#24150,#24151);
#21054=AXIS2_PLACEMENT_3D('',#29283,#24154,#24155);
#21055=AXIS2_PLACEMENT_3D('',#29284,#24156,#24157);
#21056=AXIS2_PLACEMENT_3D('',#29285,#24158,#24159);
#21057=AXIS2_PLACEMENT_3D('',#29287,#24161,#24162);
#21058=AXIS2_PLACEMENT_3D('',#29289,#24164,#24165);
#21059=AXIS2_PLACEMENT_3D('',#29290,#24166,#24167);
#21060=AXIS2_PLACEMENT_3D('',#29292,#24169,#24170);
#21061=AXIS2_PLACEMENT_3D('',#29294,#24172,#24173);
#21062=AXIS2_PLACEMENT_3D('',#29295,#24174,#24175);
#21063=AXIS2_PLACEMENT_3D('',#29297,#24177,#24178);
#21064=AXIS2_PLACEMENT_3D('',#29299,#24180,#24181);
#21065=AXIS2_PLACEMENT_3D('',#29300,#24182,#24183);
#21066=AXIS2_PLACEMENT_3D('',#29302,#24185,#24186);
#21067=AXIS2_PLACEMENT_3D('',#29304,#24188,#24189);
#21068=AXIS2_PLACEMENT_3D('',#29305,#24190,#24191);
#21069=AXIS2_PLACEMENT_3D('',#29307,#24193,#24194);
#21070=AXIS2_PLACEMENT_3D('',#29309,#24196,#24197);
#21071=AXIS2_PLACEMENT_3D('',#29310,#24198,#24199);
#21072=AXIS2_PLACEMENT_3D('',#29312,#24201,#24202);
#21073=AXIS2_PLACEMENT_3D('',#29314,#24204,#24205);
#21074=AXIS2_PLACEMENT_3D('',#29315,#24206,#24207);
#21075=AXIS2_PLACEMENT_3D('',#29317,#24209,#24210);
#21076=AXIS2_PLACEMENT_3D('',#29319,#24212,#24213);
#21077=AXIS2_PLACEMENT_3D('',#29320,#24214,#24215);
#21078=AXIS2_PLACEMENT_3D('',#29322,#24217,#24218);
#21079=AXIS2_PLACEMENT_3D('',#29324,#24220,#24221);
#23372=DIRECTION('axis',(0.,0.,1.));
#23373=DIRECTION('refdir',(1.,0.,0.));
#23374=DIRECTION('center_axis',(0.,0.,1.));
#23375=DIRECTION('ref_axis',(-1.,0.,0.));
#23376=DIRECTION('center_axis',(0.,0.,-1.));
#23377=DIRECTION('ref_axis',(-1.,0.,0.));
#23378=DIRECTION('',(0.,0.,1.));
#23379=DIRECTION('center_axis',(0.,0.,-1.));
#23380=DIRECTION('ref_axis',(-1.,0.,0.));
#23381=DIRECTION('center_axis',(0.,0.,1.));
#23382=DIRECTION('ref_axis',(-1.,0.,0.));
#23383=DIRECTION('center_axis',(0.,0.,-1.));
#23384=DIRECTION('ref_axis',(-1.,0.,0.));
#23385=DIRECTION('center_axis',(-1.22464679914735E-16,1.,0.));
#23386=DIRECTION('ref_axis',(1.,1.22464679914735E-16,0.));
#23387=DIRECTION('center_axis',(0.,0.,1.));
#23388=DIRECTION('ref_axis',(-1.,0.,0.));
#23389=DIRECTION('center_axis',(0.,0.,-1.));
#23390=DIRECTION('ref_axis',(-1.,0.,0.));
#23391=DIRECTION('center_axis',(-1.22464679914735E-16,1.,0.));
#23392=DIRECTION('ref_axis',(1.,1.22464679914735E-16,0.));
#23393=DIRECTION('center_axis',(0.,0.,-1.));
#23394=DIRECTION('ref_axis',(-1.,0.,0.));
#23395=DIRECTION('center_axis',(0.,0.,1.));
#23396=DIRECTION('ref_axis',(-1.,0.,0.));
#23397=DIRECTION('center_axis',(0.,0.,-1.));
#23398=DIRECTION('ref_axis',(-1.,0.,0.));
#23399=DIRECTION('',(-0.777743299254268,-9.52460841990042E-17,-0.628582023657284));
#23400=DIRECTION('center_axis',(0.,0.,1.));
#23401=DIRECTION('ref_axis',(-1.,0.,0.));
#23402=DIRECTION('center_axis',(0.,0.,-1.));
#23403=DIRECTION('ref_axis',(-1.04744440165294E-14,-1.,0.));
#23404=DIRECTION('center_axis',(0.,0.,-1.));
#23405=DIRECTION('ref_axis',(-1.,0.,0.));
#23406=DIRECTION('center_axis',(0.,0.,-1.));
#23407=DIRECTION('ref_axis',(-0.707106781186556,-0.707106781186539,0.));
#23408=DIRECTION('center_axis',(0.,0.,-1.));
#23409=DIRECTION('ref_axis',(-1.,0.,0.));
#23410=DIRECTION('center_axis',(0.,0.,-1.));
#23411=DIRECTION('ref_axis',(-1.,0.,0.));
#23412=DIRECTION('center_axis',(0.,0.,-1.));
#23413=DIRECTION('ref_axis',(-1.,0.,0.));
#23414=DIRECTION('center_axis',(0.,0.,-1.));
#23415=DIRECTION('ref_axis',(-0.707106781186546,0.707106781186549,0.));
#23416=DIRECTION('center_axis',(0.,0.,-1.));
#23417=DIRECTION('ref_axis',(-1.,0.,0.));
#23418=DIRECTION('center_axis',(0.,0.,-1.));
#23419=DIRECTION('ref_axis',(3.49148133884313E-15,1.,0.));
#23420=DIRECTION('center_axis',(1.22464679914735E-16,-1.,0.));
#23421=DIRECTION('ref_axis',(1.,1.22464679914735E-16,0.));
#23422=DIRECTION('center_axis',(0.,0.,-1.));
#23423=DIRECTION('ref_axis',(3.49148133884313E-15,1.,0.));
#23424=DIRECTION('center_axis',(0.,0.,-1.));
#23425=DIRECTION('ref_axis',(-1.,0.,0.));
#23426=DIRECTION('center_axis',(0.,0.,-1.));
#23427=DIRECTION('ref_axis',(0.707106781186551,0.707106781186544,0.));
#23428=DIRECTION('center_axis',(0.,0.,-1.));
#23429=DIRECTION('ref_axis',(-1.,0.,0.));
#23430=DIRECTION('center_axis',(0.,0.,-1.));
#23431=DIRECTION('ref_axis',(1.,0.,0.));
#23432=DIRECTION('center_axis',(0.,0.,-1.));
#23433=DIRECTION('ref_axis',(-1.,0.,0.));
#23434=DIRECTION('center_axis',(0.,0.,-1.));
#23435=DIRECTION('ref_axis',(0.707106781186541,-0.707106781186554,0.));
#23436=DIRECTION('center_axis',(0.,0.,-1.));
#23437=DIRECTION('ref_axis',(-1.,0.,0.));
#23438=DIRECTION('center_axis',(0.,0.,1.));
#23439=DIRECTION('ref_axis',(-1.,0.,0.));
#23440=DIRECTION('center_axis',(0.,0.,-1.));
#23441=DIRECTION('ref_axis',(-1.,0.,0.));
#23442=DIRECTION('',(0.777743299254267,9.5246084199004E-17,0.628582023657285));
#23443=DIRECTION('center_axis',(0.,0.,-1.));
#23444=DIRECTION('ref_axis',(-1.,0.,0.));
#23445=DIRECTION('center_axis',(0.,0.,1.));
#23446=DIRECTION('ref_axis',(-1.,0.,0.));
#23447=DIRECTION('center_axis',(0.,0.,-1.));
#23448=DIRECTION('ref_axis',(-1.,0.,0.));
#23449=DIRECTION('center_axis',(1.22464679914735E-16,-1.,0.));
#23450=DIRECTION('ref_axis',(1.,1.22464679914735E-16,0.));
#23451=DIRECTION('center_axis',(0.,0.,1.));
#23452=DIRECTION('ref_axis',(-1.,0.,0.));
#23453=DIRECTION('center_axis',(-1.22464679914735E-16,1.,0.));
#23454=DIRECTION('ref_axis',(1.,1.22464679914735E-16,0.));
#23455=DIRECTION('center_axis',(0.,0.,1.));
#23456=DIRECTION('ref_axis',(-3.21581820271403E-13,1.,0.));
#23457=DIRECTION('center_axis',(-2.65449697024962E-14,-1.,1.84854068675772E-14));
#23458=DIRECTION('ref_axis',(0.945228043453424,-3.1125259244975E-14,-0.326410701217364));
#23459=DIRECTION('center_axis',(0.,0.,-1.));
#23460=DIRECTION('ref_axis',(-1.,0.,0.));
#23461=DIRECTION('center_axis',(-0.707106781186532,0.707106781186563,-1.36879902392314E-14));
#23462=DIRECTION('ref_axis',(0.241837082303472,0.241837082303443,-0.939696574031161));
#23463=DIRECTION('center_axis',(0.,0.,1.));
#23464=DIRECTION('ref_axis',(-0.707106781186489,0.707106781186606,0.));
#23465=DIRECTION('center_axis',(0.707106781186527,-0.707106781186568,2.46702181021724E-14));
#23466=DIRECTION('ref_axis',(0.668377159293632,0.668377159293584,-0.326410701217368));
#23467=DIRECTION('center_axis',(0.,0.,-1.));
#23468=DIRECTION('ref_axis',(-1.,0.,0.));
#23469=DIRECTION('center_axis',(-1.,-1.65009199484293E-15,1.71165480509254E-15));
#23470=DIRECTION('ref_axis',(-2.1746906207308E-15,0.342009281678289,-0.939696574031161));
#23471=DIRECTION('center_axis',(0.,0.,1.));
#23472=DIRECTION('ref_axis',(-1.,8.08242361927114E-14,0.));
#23473=DIRECTION('center_axis',(1.,-1.15612551933786E-14,1.13714767015716E-14));
#23474=DIRECTION('ref_axis',(1.46383861165231E-14,0.945228043453423,-0.326410701217368));
#23475=DIRECTION('center_axis',(0.,0.,-1.));
#23476=DIRECTION('ref_axis',(-1.,0.,0.));
#23477=DIRECTION('center_axis',(-0.707106781186545,-0.70710678118655,1.49612916568344E-14));
#23478=DIRECTION('ref_axis',(-0.24183708230347,0.241837082303447,-0.939696574031161));
#23479=DIRECTION('center_axis',(0.,0.,1.));
#23480=DIRECTION('ref_axis',(-0.707106781186613,-0.707106781186482,0.));
#23481=DIRECTION('center_axis',(0.707106781186564,0.707106781186531,1.16188769126359E-14));
#23482=DIRECTION('ref_axis',(-0.66837715929359,0.668377159293628,-0.326410701217364));
#23483=DIRECTION('center_axis',(0.,0.,-1.));
#23484=DIRECTION('ref_axis',(-1.,0.,0.));
#23485=DIRECTION('center_axis',(-1.0700730164861E-14,-1.,-6.44787115032575E-17));
#23486=DIRECTION('ref_axis',(-0.342009281678279,3.72415768800159E-15,-0.939696574031164));
#23487=DIRECTION('center_axis',(0.,0.,1.));
#23488=DIRECTION('ref_axis',(-4.98084396431898E-13,-1.,0.));
#23489=DIRECTION('center_axis',(1.02700574112875E-14,1.,-4.88525407613946E-17));
#23490=DIRECTION('ref_axis',(-0.945228043453422,9.69096499636107E-15,-0.326410701217372));
#23491=DIRECTION('center_axis',(0.,0.,-1.));
#23492=DIRECTION('ref_axis',(-1.,0.,0.));
#23493=DIRECTION('center_axis',(0.707106781186529,-0.707106781186566,-1.90995212640436E-14));
#23494=DIRECTION('ref_axis',(-0.241837082303473,-0.241837082303435,-0.939696574031163));
#23495=DIRECTION('center_axis',(0.,0.,1.));
#23496=DIRECTION('ref_axis',(0.707106781186484,-0.707106781186611,0.));
#23497=DIRECTION('center_axis',(-0.707106781186538,0.707106781186557,4.77488092300106E-15));
#23498=DIRECTION('ref_axis',(-0.668377159293619,-0.6683771592936,-0.326410701217363));
#23499=DIRECTION('center_axis',(0.,0.,-1.));
#23500=DIRECTION('ref_axis',(-1.,0.,0.));
#23501=DIRECTION('center_axis',(1.,1.79398764678015E-15,1.76453926386396E-15));
#23502=DIRECTION('ref_axis',(2.26983333538778E-15,-0.342009281678289,-0.939696574031161));
#23503=DIRECTION('center_axis',(0.,0.,1.));
#23504=DIRECTION('ref_axis',(1.,-8.08242361927114E-14,0.));
#23505=DIRECTION('center_axis',(-1.,-7.91804511680167E-15,-7.69942093215295E-15));
#23506=DIRECTION('ref_axis',(1.00035767704373E-14,-0.945228043453423,-0.326410701217368));
#23507=DIRECTION('center_axis',(0.,0.,-1.));
#23508=DIRECTION('ref_axis',(-1.,0.,0.));
#23509=DIRECTION('center_axis',(0.707106781186536,0.707106781186559,1.97361719728453E-14));
#23510=DIRECTION('ref_axis',(0.241837082303476,-0.241837082303441,-0.939696574031161));
#23511=DIRECTION('center_axis',(0.,0.,1.));
#23512=DIRECTION('ref_axis',(0.707106781186608,0.707106781186487,0.));
#23513=DIRECTION('center_axis',(-0.707106781186538,-0.707106781186557,-2.18052895483717E-14));
#23514=DIRECTION('ref_axis',(0.668377159293621,-0.668377159293593,-0.326410701217372));
#23515=DIRECTION('center_axis',(0.,0.,-1.));
#23516=DIRECTION('ref_axis',(-1.,0.,0.));
#23517=DIRECTION('center_axis',(-6.13527734841807E-15,1.,1.38135285440519E-14));
#23518=DIRECTION('ref_axis',(0.342009281678287,1.50733243649404E-14,-0.939696574031162));
#23519=DIRECTION('center_axis',(0.,0.,1.));
#23520=DIRECTION('ref_axis',(-3.21581820271403E-13,1.,0.));
#23521=DIRECTION('center_axis',(0.,0.,1.));
#23522=DIRECTION('ref_axis',(-1.,0.,0.));
#23523=DIRECTION('',(0.664464832747924,-0.664464832747934,0.34201311682819));
#23524=DIRECTION('center_axis',(0.,0.,-1.));
#23525=DIRECTION('ref_axis',(-1.,0.,0.));
#23526=DIRECTION('',(-0.93969517819209,3.34165038880862E-15,-0.342013116828193));
#23527=DIRECTION('center_axis',(0.,0.,1.));
#23528=DIRECTION('ref_axis',(-1.,0.,0.));
#23529=DIRECTION('center_axis',(0.,0.,-1.));
#23530=DIRECTION('ref_axis',(-1.,0.,0.));
#23531=DIRECTION('',(-0.664464832747918,-0.664464832747939,-0.342013116828193));
#23532=DIRECTION('',(0.93969517819209,-3.2601467207889E-15,0.342013116828193));
#23533=DIRECTION('center_axis',(0.,0.,1.));
#23534=DIRECTION('ref_axis',(-1.,0.,0.));
#23535=DIRECTION('',(8.15036680197226E-17,-0.93969517819209,0.342013116828193));
#23536=DIRECTION('center_axis',(0.,0.,-1.));
#23537=DIRECTION('ref_axis',(-1.,0.,0.));
#23538=DIRECTION('',(-0.664464832747928,0.664464832747928,-0.342013116828193));
#23539=DIRECTION('center_axis',(0.,0.,1.));
#23540=DIRECTION('ref_axis',(-1.,0.,0.));
#23541=DIRECTION('',(-0.66446483274794,-0.664464832747919,0.342013116828188));
#23542=DIRECTION('center_axis',(0.,0.,-1.));
#23543=DIRECTION('ref_axis',(-1.,0.,0.));
#23544=DIRECTION('',(8.15036680197226E-17,0.93969517819209,-0.342013116828193));
#23545=DIRECTION('center_axis',(0.,0.,1.));
#23546=DIRECTION('ref_axis',(-1.,0.,0.));
#23547=DIRECTION('',(-0.93969517819209,9.78044016236671E-15,0.342013116828193));
#23548=DIRECTION('center_axis',(0.,0.,-1.));
#23549=DIRECTION('ref_axis',(-1.,0.,0.));
#23550=DIRECTION('',(0.664464832747934,0.664464832747924,-0.34201311682819));
#23551=DIRECTION('center_axis',(0.,0.,1.));
#23552=DIRECTION('ref_axis',(-1.,0.,0.));
#23553=DIRECTION('',(-0.664464832747918,0.664464832747939,0.342013116828193));
#23554=DIRECTION('center_axis',(0.,0.,-1.));
#23555=DIRECTION('ref_axis',(-1.,0.,0.));
#23556=DIRECTION('',(0.939695178192092,-9.94344749840606E-15,-0.34201311682819));
#23557=DIRECTION('center_axis',(0.,0.,1.));
#23558=DIRECTION('ref_axis',(-1.,0.,0.));
#23559=DIRECTION('',(-8.15036680197226E-17,0.93969517819209,0.342013116828193));
#23560=DIRECTION('center_axis',(0.,0.,-1.));
#23561=DIRECTION('ref_axis',(-1.,0.,0.));
#23562=DIRECTION('',(0.664464832747918,-0.664464832747939,-0.342013116828193));
#23563=DIRECTION('center_axis',(0.,0.,1.));
#23564=DIRECTION('ref_axis',(-1.,0.,0.));
#23565=DIRECTION('center_axis',(0.,0.,-1.));
#23566=DIRECTION('ref_axis',(-1.,0.,0.));
#23567=DIRECTION('',(-8.15036680197226E-17,-0.93969517819209,-0.342013116828193));
#23568=DIRECTION('',(0.664464832747934,0.664464832747924,0.34201311682819));
#23569=DIRECTION('center_axis',(0.,0.,-1.));
#23570=DIRECTION('ref_axis',(1.,0.,0.));
#23571=DIRECTION('',(0.241849828089742,-0.241849828089742,-0.939690013411829));
#23572=DIRECTION('center_axis',(0.,0.,-1.));
#23573=DIRECTION('ref_axis',(-1.,0.,0.));
#23574=DIRECTION('',(-0.342027306942117,1.29765967489722E-15,0.939690013411829));
#23575=DIRECTION('center_axis',(0.,0.,-1.));
#23576=DIRECTION('ref_axis',(1.,0.,0.));
#23577=DIRECTION('center_axis',(0.,0.,-1.));
#23578=DIRECTION('ref_axis',(-1.,0.,0.));
#23579=DIRECTION('',(-0.241849828089751,-0.241849828089742,0.939690013411827));
#23580=DIRECTION('',(0.342027306942117,-1.08138306241435E-15,-0.939690013411829));
#23581=DIRECTION('center_axis',(0.,0.,-1.));
#23582=DIRECTION('ref_axis',(1.,0.,0.));
#23583=DIRECTION('',(7.20922041609565E-17,-0.342027306942117,-0.939690013411829));
#23584=DIRECTION('center_axis',(0.,0.,-1.));
#23585=DIRECTION('ref_axis',(-1.,0.,0.));
#23586=DIRECTION('',(-0.241849828089734,0.241849828089743,0.939690013411832));
#23587=DIRECTION('center_axis',(0.,0.,-1.));
#23588=DIRECTION('ref_axis',(1.,0.,0.));
#23589=DIRECTION('',(-0.241849828089734,-0.241849828089743,-0.939690013411832));
#23590=DIRECTION('center_axis',(0.,0.,-1.));
#23591=DIRECTION('ref_axis',(-1.,0.,0.));
#23592=DIRECTION('',(7.20922041609565E-17,0.342027306942117,0.939690013411829));
#23593=DIRECTION('center_axis',(0.,0.,-1.));
#23594=DIRECTION('ref_axis',(1.,0.,0.));
#23595=DIRECTION('',(-0.342027306942125,3.4604257997259E-15,-0.939690013411826));
#23596=DIRECTION('center_axis',(0.,0.,-1.));
#23597=DIRECTION('ref_axis',(-1.,0.,0.));
#23598=DIRECTION('',(0.241849828089751,0.241849828089742,0.939690013411827));
#23599=DIRECTION('center_axis',(0.,0.,-1.));
#23600=DIRECTION('ref_axis',(1.,0.,0.));
#23601=DIRECTION('',(-0.241849828089742,0.241849828089751,-0.939690013411827));
#23602=DIRECTION('center_axis',(0.,0.,-1.));
#23603=DIRECTION('ref_axis',(-1.,0.,0.));
#23604=DIRECTION('',(0.342027306942117,-3.74879461636974E-15,0.939690013411829));
#23605=DIRECTION('center_axis',(0.,0.,-1.));
#23606=DIRECTION('ref_axis',(1.,0.,0.));
#23607=DIRECTION('',(-7.20922041609565E-17,0.342027306942117,-0.939690013411829));
#23608=DIRECTION('center_axis',(0.,0.,-1.));
#23609=DIRECTION('ref_axis',(-1.,0.,0.));
#23610=DIRECTION('',(0.241849828089733,-0.241849828089752,0.939690013411829));
#23611=DIRECTION('center_axis',(0.,0.,-1.));
#23612=DIRECTION('ref_axis',(1.,0.,0.));
#23613=DIRECTION('center_axis',(0.,0.,-1.));
#23614=DIRECTION('ref_axis',(-1.,0.,0.));
#23615=DIRECTION('',(-7.20922041609565E-17,-0.342027306942117,0.939690013411829));
#23616=DIRECTION('',(0.241849828089734,0.241849828089743,-0.939690013411832));
#23617=DIRECTION('center_axis',(0.,0.,1.));
#23618=DIRECTION('ref_axis',(-1.,0.,0.));
#23619=DIRECTION('',(-0.405586087801291,0.405586087801293,-0.819145805558501));
#23620=DIRECTION('',(0.573585346078431,-2.07701987415471E-15,0.819145805558501));
#23621=DIRECTION('center_axis',(0.,0.,1.));
#23622=DIRECTION('ref_axis',(-1.,0.,0.));
#23623=DIRECTION('',(0.405586087801295,0.405586087801293,0.819145805558499));
#23624=DIRECTION('',(-0.573585346078431,1.91898575329511E-15,-0.819145805558501));
#23625=DIRECTION('center_axis',(0.,0.,1.));
#23626=DIRECTION('ref_axis',(-1.,0.,0.));
#23627=DIRECTION('',(-6.77289089398275E-17,0.573585346078431,-0.819145805558501));
#23628=DIRECTION('',(0.405586087801291,-0.405586087801293,0.819145805558501));
#23629=DIRECTION('center_axis',(0.,0.,1.));
#23630=DIRECTION('ref_axis',(-1.,0.,0.));
#23631=DIRECTION('',(0.405586087801294,0.405586087801288,-0.819145805558502));
#23632=DIRECTION('',(-9.030521191977E-17,-0.573585346078431,0.819145805558501));
#23633=DIRECTION('center_axis',(0.,0.,1.));
#23634=DIRECTION('ref_axis',(-1.,0.,0.));
#23635=DIRECTION('',(0.573585346078431,-5.93756768372488E-15,-0.819145805558501));
#23636=DIRECTION('',(-0.405586087801298,-0.40558608780129,0.819145805558499));
#23637=DIRECTION('center_axis',(0.,0.,1.));
#23638=DIRECTION('ref_axis',(-1.,0.,0.));
#23639=DIRECTION('',(0.405586087801288,-0.405586087801296,-0.819145805558501));
#23640=DIRECTION('',(-0.573585346078433,6.11817810756441E-15,0.8191458055585));
#23641=DIRECTION('center_axis',(0.,0.,1.));
#23642=DIRECTION('ref_axis',(-1.,0.,0.));
#23643=DIRECTION('',(6.77289089398275E-17,-0.573585346078431,-0.819145805558501));
#23644=DIRECTION('',(-0.405586087801287,0.405586087801299,0.8191458055585));
#23645=DIRECTION('center_axis',(0.,0.,1.));
#23646=DIRECTION('ref_axis',(-1.,0.,0.));
#23647=DIRECTION('',(9.030521191977E-17,0.573585346078431,0.819145805558501));
#23648=DIRECTION('',(-0.405586087801294,-0.405586087801288,-0.819145805558502));
#23649=DIRECTION('center_axis',(0.,0.,-1.));
#23650=DIRECTION('ref_axis',(1.,0.,0.));
#23651=DIRECTION('center_axis',(0.,0.,1.));
#23652=DIRECTION('ref_axis',(-1.,0.,0.));
#23653=DIRECTION('center_axis',(-1.,1.27191845719472E-16,0.));
#23654=DIRECTION('ref_axis',(-1.27191845719472E-16,-1.,0.));
#23655=DIRECTION('',(1.27191845719472E-16,1.,0.));
#23656=DIRECTION('center_axis',(1.,1.27191845719472E-16,0.));
#23657=DIRECTION('ref_axis',(-1.27191845719472E-16,1.,0.));
#23658=DIRECTION('',(1.27191845719472E-16,-1.,0.));
#23659=DIRECTION('center_axis',(0.,0.,1.));
#23660=DIRECTION('ref_axis',(-1.,0.,0.));
#23661=DIRECTION('center_axis',(-0.707106781186546,0.707106781186549,0.));
#23662=DIRECTION('ref_axis',(-0.707106781186549,-0.707106781186546,0.));
#23663=DIRECTION('',(0.707106781186549,0.707106781186546,0.));
#23664=DIRECTION('center_axis',(0.707106781186546,-0.707106781186549,0.));
#23665=DIRECTION('ref_axis',(0.707106781186549,0.707106781186546,0.));
#23666=DIRECTION('',(-0.707106781186549,-0.707106781186546,0.));
#23667=DIRECTION('center_axis',(0.,0.,1.));
#23668=DIRECTION('ref_axis',(-0.707106781186546,0.707106781186549,0.));
#23669=DIRECTION('center_axis',(-0.707106781186556,-0.707106781186539,0.));
#23670=DIRECTION('ref_axis',(0.707106781186539,-0.707106781186556,0.));
#23671=DIRECTION('',(-0.707106781186539,0.707106781186556,0.));
#23672=DIRECTION('center_axis',(0.707106781186556,0.707106781186539,0.));
#23673=DIRECTION('ref_axis',(-0.707106781186539,0.707106781186556,0.));
#23674=DIRECTION('',(0.707106781186539,-0.707106781186556,0.));
#23675=DIRECTION('center_axis',(0.,0.,1.));
#23676=DIRECTION('ref_axis',(-0.707106781186556,-0.707106781186539,0.));
#23677=DIRECTION('center_axis',(-1.06016358622489E-14,-1.,0.));
#23678=DIRECTION('ref_axis',(1.,-1.06016358622489E-14,0.));
#23679=DIRECTION('',(-1.,1.06016358622489E-14,0.));
#23680=DIRECTION('center_axis',(1.03472521708099E-14,1.,0.));
#23681=DIRECTION('ref_axis',(-1.,1.03472521708099E-14,0.));
#23682=DIRECTION('',(1.,-1.03472521708099E-14,0.));
#23683=DIRECTION('center_axis',(0.,0.,1.));
#23684=DIRECTION('ref_axis',(-1.04744440165294E-14,-1.,0.));
#23685=DIRECTION('center_axis',(0.707106781186541,-0.707106781186554,0.));
#23686=DIRECTION('ref_axis',(0.707106781186554,0.707106781186541,0.));
#23687=DIRECTION('',(-0.707106781186554,-0.707106781186541,0.));
#23688=DIRECTION('center_axis',(-0.707106781186541,0.707106781186554,0.));
#23689=DIRECTION('ref_axis',(-0.707106781186554,-0.707106781186541,0.));
#23690=DIRECTION('',(0.707106781186554,0.707106781186541,0.));
#23691=DIRECTION('center_axis',(0.,0.,1.));
#23692=DIRECTION('ref_axis',(0.707106781186541,-0.707106781186554,0.));
#23693=DIRECTION('center_axis',(1.,-1.27191845719472E-16,0.));
#23694=DIRECTION('ref_axis',(1.27191845719472E-16,1.,0.));
#23695=DIRECTION('',(-1.27191845719472E-16,-1.,0.));
#23696=DIRECTION('center_axis',(-1.,-1.27191845719472E-16,0.));
#23697=DIRECTION('ref_axis',(1.27191845719472E-16,-1.,0.));
#23698=DIRECTION('',(-1.27191845719472E-16,1.,0.));
#23699=DIRECTION('center_axis',(0.,0.,1.));
#23700=DIRECTION('ref_axis',(1.,0.,0.));
#23701=DIRECTION('center_axis',(0.707106781186551,0.707106781186544,0.));
#23702=DIRECTION('ref_axis',(-0.707106781186544,0.707106781186551,0.));
#23703=DIRECTION('',(0.707106781186544,-0.707106781186551,0.));
#23704=DIRECTION('center_axis',(-0.707106781186551,-0.707106781186544,0.));
#23705=DIRECTION('ref_axis',(0.707106781186544,-0.707106781186551,0.));
#23706=DIRECTION('',(-0.707106781186544,0.707106781186551,0.));
#23707=DIRECTION('center_axis',(0.,0.,1.));
#23708=DIRECTION('ref_axis',(0.707106781186551,0.707106781186544,0.));
#23709=DIRECTION('center_axis',(3.61867318456261E-15,1.,0.));
#23710=DIRECTION('ref_axis',(-1.,3.61867318456261E-15,0.));
#23711=DIRECTION('',(1.,-3.61867318456261E-15,0.));
#23712=DIRECTION('center_axis',(-3.36428949312366E-15,-1.,0.));
#23713=DIRECTION('ref_axis',(1.,-3.36428949312366E-15,0.));
#23714=DIRECTION('',(-1.,3.36428949312366E-15,0.));
#23715=DIRECTION('center_axis',(0.,0.,1.));
#23716=DIRECTION('ref_axis',(3.49148133884313E-15,1.,0.));
#23717=DIRECTION('center_axis',(1.,0.,6.12323399573677E-17));
#23718=DIRECTION('ref_axis',(0.,0.,1.));
#23719=DIRECTION('center_axis',(0.,1.,0.));
#23720=DIRECTION('ref_axis',(0.,0.,-1.));
#23721=DIRECTION('center_axis',(0.,0.,1.));
#23722=DIRECTION('ref_axis',(1.,0.,0.));
#23723=DIRECTION('center_axis',(0.,0.,-1.));
#23724=DIRECTION('ref_axis',(-1.,0.,0.));
#23725=DIRECTION('center_axis',(-1.22464679914735E-16,1.,0.));
#23726=DIRECTION('ref_axis',(-1.,-1.22464679914735E-16,0.));
#23727=DIRECTION('center_axis',(0.,0.,1.));
#23728=DIRECTION('ref_axis',(1.,0.,0.));
#23729=DIRECTION('center_axis',(0.,0.,1.));
#23730=DIRECTION('ref_axis',(1.,0.,0.));
#23731=DIRECTION('center_axis',(0.,0.,1.));
#23732=DIRECTION('ref_axis',(1.,0.,0.));
#23733=DIRECTION('center_axis',(1.22464679914735E-16,-1.,0.));
#23734=DIRECTION('ref_axis',(-1.,-1.22464679914735E-16,0.));
#23735=DIRECTION('center_axis',(0.,0.,1.));
#23736=DIRECTION('ref_axis',(1.,0.,0.));
#23737=DIRECTION('center_axis',(0.,0.,1.));
#23738=DIRECTION('ref_axis',(1.,0.,0.));
#23739=DIRECTION('center_axis',(0.,0.,-1.));
#23740=DIRECTION('ref_axis',(-1.,0.,0.));
#23741=DIRECTION('center_axis',(0.,0.,1.));
#23742=DIRECTION('ref_axis',(1.,0.,0.));
#23743=DIRECTION('',(0.12186934340514,-1.49246901315294E-17,-0.992546151641323));
#23744=DIRECTION('center_axis',(0.,0.,1.));
#23745=DIRECTION('ref_axis',(1.,0.,0.));
#23746=DIRECTION('center_axis',(0.,0.,1.));
#23747=DIRECTION('ref_axis',(1.,0.,0.));
#23748=DIRECTION('',(0.,0.,1.));
#23749=DIRECTION('center_axis',(0.,0.,1.));
#23750=DIRECTION('ref_axis',(1.,0.,0.));
#23751=DIRECTION('center_axis',(0.,0.,1.));
#23752=DIRECTION('ref_axis',(1.,0.,0.));
#23753=DIRECTION('',(-0.12186934340514,-1.49246901315294E-17,0.992546151641323));
#23754=DIRECTION('center_axis',(0.,0.,1.));
#23755=DIRECTION('ref_axis',(1.,0.,0.));
#23756=DIRECTION('center_axis',(0.,0.,1.));
#23757=DIRECTION('ref_axis',(1.,0.,0.));
#23758=DIRECTION('center_axis',(1.22464679914735E-16,-1.,0.));
#23759=DIRECTION('ref_axis',(-1.,-1.22464679914735E-16,0.));
#23760=DIRECTION('center_axis',(0.,0.,1.));
#23761=DIRECTION('ref_axis',(1.,0.,0.));
#23762=DIRECTION('center_axis',(0.,0.,1.));
#23763=DIRECTION('ref_axis',(1.,0.,0.));
#23764=DIRECTION('center_axis',(0.,0.,1.));
#23765=DIRECTION('ref_axis',(1.,0.,0.));
#23766=DIRECTION('center_axis',(1.22464679914735E-16,-1.,0.));
#23767=DIRECTION('ref_axis',(-1.,-1.22464679914735E-16,0.));
#23768=DIRECTION('center_axis',(0.,0.,1.));
#23769=DIRECTION('ref_axis',(1.,0.,0.));
#23770=DIRECTION('center_axis',(0.,0.,1.));
#23771=DIRECTION('ref_axis',(1.,0.,0.));
#23772=DIRECTION('center_axis',(0.,0.,1.));
#23773=DIRECTION('ref_axis',(1.,0.,0.));
#23774=DIRECTION('center_axis',(1.22464679914735E-16,-1.,0.));
#23775=DIRECTION('ref_axis',(-1.,-1.22464679914735E-16,0.));
#23776=DIRECTION('center_axis',(0.,0.,1.));
#23777=DIRECTION('ref_axis',(1.,0.,0.));
#23778=DIRECTION('center_axis',(0.,0.,1.));
#23779=DIRECTION('ref_axis',(1.,0.,0.));
#23780=DIRECTION('',(0.,0.,-1.));
#23781=DIRECTION('center_axis',(0.,0.,1.));
#23782=DIRECTION('ref_axis',(1.,0.,0.));
#23783=DIRECTION('',(0.,0.,-1.));
#23784=DIRECTION('center_axis',(0.,0.,-1.));
#23785=DIRECTION('ref_axis',(-1.,0.,0.));
#23786=DIRECTION('center_axis',(0.,0.,1.));
#23787=DIRECTION('ref_axis',(1.,0.,0.));
#23788=DIRECTION('center_axis',(0.,0.,1.));
#23789=DIRECTION('ref_axis',(1.,0.,0.));
#23790=DIRECTION('center_axis',(0.,0.,-1.));
#23791=DIRECTION('ref_axis',(1.,0.,0.));
#23792=DIRECTION('center_axis',(-1.22464679914735E-16,1.,0.));
#23793=DIRECTION('ref_axis',(-1.,-1.22464679914735E-16,0.));
#23794=DIRECTION('center_axis',(0.,0.,1.));
#23795=DIRECTION('ref_axis',(-1.,0.,0.));
#23796=DIRECTION('center_axis',(0.,0.,1.));
#23797=DIRECTION('ref_axis',(1.,0.,0.));
#23798=DIRECTION('center_axis',(0.,0.,1.));
#23799=DIRECTION('ref_axis',(1.,0.,0.));
#23800=DIRECTION('',(0.,0.,-1.));
#23801=DIRECTION('center_axis',(0.,0.,1.));
#23802=DIRECTION('ref_axis',(1.,0.,0.));
#23803=DIRECTION('center_axis',(0.,0.,1.));
#23804=DIRECTION('ref_axis',(1.,0.,0.));
#23805=DIRECTION('center_axis',(1.22464679914735E-16,-1.,0.));
#23806=DIRECTION('ref_axis',(-1.,-1.22464679914735E-16,0.));
#23807=DIRECTION('center_axis',(0.,0.,1.));
#23808=DIRECTION('ref_axis',(1.,0.,0.));
#23809=DIRECTION('center_axis',(0.,0.,1.));
#23810=DIRECTION('ref_axis',(1.,0.,0.));
#23811=DIRECTION('',(0.992546151641321,1.21551846761357E-16,-0.121869343405157));
#23812=DIRECTION('center_axis',(0.,0.,1.));
#23813=DIRECTION('ref_axis',(1.,0.,0.));
#23814=DIRECTION('center_axis',(0.,0.,-1.));
#23815=DIRECTION('ref_axis',(-1.,0.,0.));
#23816=DIRECTION('center_axis',(0.,0.,1.));
#23817=DIRECTION('ref_axis',(1.,0.,0.));
#23818=DIRECTION('',(-0.992546151641322,1.21551846761357E-16,0.121869343405149));
#23819=DIRECTION('center_axis',(0.,0.,1.));
#23820=DIRECTION('ref_axis',(1.,0.,0.));
#23821=DIRECTION('center_axis',(0.,0.,1.));
#23822=DIRECTION('ref_axis',(1.,0.,0.));
#23823=DIRECTION('center_axis',(0.,0.,1.));
#23824=DIRECTION('ref_axis',(1.,0.,0.));
#23825=DIRECTION('center_axis',(1.22464679914735E-16,-1.,0.));
#23826=DIRECTION('ref_axis',(-1.,-1.22464679914735E-16,0.));
#23827=DIRECTION('center_axis',(0.,0.,1.));
#23828=DIRECTION('ref_axis',(1.,0.,0.));
#23829=DIRECTION('center_axis',(0.,0.,1.));
#23830=DIRECTION('ref_axis',(1.,0.,0.));
#23831=DIRECTION('',(0.,0.,1.));
#23832=DIRECTION('center_axis',(0.,0.,1.));
#23833=DIRECTION('ref_axis',(1.,0.,0.));
#23834=DIRECTION('',(0.,0.,1.));
#23835=DIRECTION('center_axis',(0.,0.,1.));
#23836=DIRECTION('ref_axis',(1.,0.,0.));
#23837=DIRECTION('center_axis',(0.,0.,-1.));
#23838=DIRECTION('ref_axis',(-1.,0.,0.));
#23839=DIRECTION('center_axis',(0.,0.,1.));
#23840=DIRECTION('ref_axis',(1.,0.,0.));
#23841=DIRECTION('center_axis',(0.707106781186546,-0.707106781186549,6.12323399573677E-17));
#23842=DIRECTION('ref_axis',(0.,0.,1.));
#23843=DIRECTION('center_axis',(0.707106781186549,0.707106781186546,0.));
#23844=DIRECTION('ref_axis',(0.,0.,-1.));
#23845=DIRECTION('center_axis',(-3.71222327254256E-15,-1.,6.12323399573677E-17));
#23846=DIRECTION('ref_axis',(0.,0.,1.));
#23847=DIRECTION('center_axis',(1.,-3.49148133884313E-15,0.));
#23848=DIRECTION('ref_axis',(0.,0.,-1.));
#23849=DIRECTION('center_axis',(-0.707106781186551,-0.707106781186544,6.12323399573676E-17));
#23850=DIRECTION('ref_axis',(0.,0.,1.));
#23851=DIRECTION('center_axis',(0.707106781186544,-0.707106781186551,0.));
#23852=DIRECTION('ref_axis',(0.,0.,-1.));
#23853=DIRECTION('center_axis',(-1.,0.,6.12323399573677E-17));
#23854=DIRECTION('ref_axis',(0.,0.,1.));
#23855=DIRECTION('center_axis',(0.,-1.,0.));
#23856=DIRECTION('ref_axis',(0.,0.,-1.));
#23857=DIRECTION('center_axis',(-0.707106781186541,0.707106781186554,6.12323399573677E-17));
#23858=DIRECTION('ref_axis',(0.,0.,1.));
#23859=DIRECTION('center_axis',(-0.707106781186554,-0.707106781186541,0.));
#23860=DIRECTION('ref_axis',(0.,0.,-1.));
#23861=DIRECTION('center_axis',(1.06726419085599E-14,1.,6.12323399573677E-17));
#23862=DIRECTION('ref_axis',(0.,0.,1.));
#23863=DIRECTION('center_axis',(-1.,1.04744440165294E-14,0.));
#23864=DIRECTION('ref_axis',(0.,0.,-1.));
#23865=DIRECTION('center_axis',(0.707106781186556,0.707106781186539,6.12323399573677E-17));
#23866=DIRECTION('ref_axis',(0.,0.,1.));
#23867=DIRECTION('center_axis',(-0.707106781186539,0.707106781186556,0.));
#23868=DIRECTION('ref_axis',(0.,0.,-1.));
#23869=DIRECTION('center_axis',(0.,0.,1.));
#23870=DIRECTION('ref_axis',(1.,0.,0.));
#23871=DIRECTION('center_axis',(0.,0.,1.));
#23872=DIRECTION('ref_axis',(-1.,0.,0.));
#23873=DIRECTION('center_axis',(0.,0.,1.));
#23874=DIRECTION('ref_axis',(-1.,0.,0.));
#23875=DIRECTION('center_axis',(-1.22464679914735E-16,1.,0.));
#23876=DIRECTION('ref_axis',(-1.,-1.22464679914735E-16,0.));
#23877=DIRECTION('center_axis',(0.,0.,-1.));
#23878=DIRECTION('ref_axis',(-1.,0.,0.));
#23879=DIRECTION('center_axis',(0.,0.,-1.));
#23880=DIRECTION('ref_axis',(-1.,0.,0.));
#23881=DIRECTION('center_axis',(0.,0.,-1.));
#23882=DIRECTION('ref_axis',(-1.,0.,0.));
#23883=DIRECTION('center_axis',(0.,0.,-1.));
#23884=DIRECTION('ref_axis',(-1.,0.,0.));
#23885=DIRECTION('',(0.,0.,-1.));
#23886=DIRECTION('center_axis',(0.,0.,-1.));
#23887=DIRECTION('ref_axis',(-1.,0.,0.));
#23888=DIRECTION('center_axis',(0.,0.,-1.));
#23889=DIRECTION('ref_axis',(-1.,0.,0.));
#23890=DIRECTION('center_axis',(0.,0.,-1.));
#23891=DIRECTION('ref_axis',(-1.,0.,0.));
#23892=DIRECTION('center_axis',(-1.22464679914735E-16,-1.,0.));
#23893=DIRECTION('ref_axis',(1.,-1.22464679914735E-16,0.));
#23894=DIRECTION('center_axis',(0.,0.,-1.));
#23895=DIRECTION('ref_axis',(-1.,0.,0.));
#23896=DIRECTION('center_axis',(0.,0.,-1.));
#23897=DIRECTION('ref_axis',(-1.,0.,0.));
#23898=DIRECTION('center_axis',(-1.22464679914735E-16,-1.,0.));
#23899=DIRECTION('ref_axis',(1.,-1.22464679914735E-16,0.));
#23900=DIRECTION('center_axis',(0.,0.,-1.));
#23901=DIRECTION('ref_axis',(-1.,0.,0.));
#23902=DIRECTION('center_axis',(0.,0.,-1.));
#23903=DIRECTION('ref_axis',(-1.,0.,0.));
#23904=DIRECTION('center_axis',(0.,0.,-1.));
#23905=DIRECTION('ref_axis',(-1.,0.,0.));
#23906=DIRECTION('',(-0.777743299254268,9.52460841990042E-17,0.628582023657284));
#23907=DIRECTION('center_axis',(0.,0.,-1.));
#23908=DIRECTION('ref_axis',(-1.,0.,0.));
#23909=DIRECTION('center_axis',(0.,0.,-1.));
#23910=DIRECTION('ref_axis',(-1.04744440165294E-14,-1.,0.));
#23911=DIRECTION('center_axis',(0.,0.,-1.));
#23912=DIRECTION('ref_axis',(-1.,0.,0.));
#23913=DIRECTION('center_axis',(0.,0.,-1.));
#23914=DIRECTION('ref_axis',(0.707106781186541,-0.707106781186554,0.));
#23915=DIRECTION('center_axis',(0.,0.,-1.));
#23916=DIRECTION('ref_axis',(-1.,0.,0.));
#23917=DIRECTION('center_axis',(0.,0.,-1.));
#23918=DIRECTION('ref_axis',(1.,0.,0.));
#23919=DIRECTION('center_axis',(0.,0.,-1.));
#23920=DIRECTION('ref_axis',(-1.,0.,0.));
#23921=DIRECTION('center_axis',(0.,0.,-1.));
#23922=DIRECTION('ref_axis',(0.707106781186551,0.707106781186544,0.));
#23923=DIRECTION('center_axis',(0.,0.,-1.));
#23924=DIRECTION('ref_axis',(-1.,0.,0.));
#23925=DIRECTION('center_axis',(0.,0.,-1.));
#23926=DIRECTION('ref_axis',(3.49148133884313E-15,1.,0.));
#23927=DIRECTION('center_axis',(1.22464679914735E-16,1.,0.));
#23928=DIRECTION('ref_axis',(1.,-1.22464679914735E-16,0.));
#23929=DIRECTION('center_axis',(0.,0.,-1.));
#23930=DIRECTION('ref_axis',(3.49148133884313E-15,1.,0.));
#23931=DIRECTION('center_axis',(0.,0.,-1.));
#23932=DIRECTION('ref_axis',(-1.,0.,0.));
#23933=DIRECTION('center_axis',(0.,0.,-1.));
#23934=DIRECTION('ref_axis',(-0.707106781186546,0.707106781186549,0.));
#23935=DIRECTION('center_axis',(0.,0.,-1.));
#23936=DIRECTION('ref_axis',(-1.,0.,0.));
#23937=DIRECTION('center_axis',(0.,0.,-1.));
#23938=DIRECTION('ref_axis',(-1.,0.,0.));
#23939=DIRECTION('center_axis',(0.,0.,-1.));
#23940=DIRECTION('ref_axis',(-1.,0.,0.));
#23941=DIRECTION('center_axis',(0.,0.,-1.));
#23942=DIRECTION('ref_axis',(-0.707106781186556,-0.707106781186539,0.));
#23943=DIRECTION('center_axis',(0.,0.,-1.));
#23944=DIRECTION('ref_axis',(-1.,0.,0.));
#23945=DIRECTION('center_axis',(0.,0.,-1.));
#23946=DIRECTION('ref_axis',(-1.,0.,0.));
#23947=DIRECTION('center_axis',(0.,0.,-1.));
#23948=DIRECTION('ref_axis',(-1.,0.,0.));
#23949=DIRECTION('center_axis',(1.22464679914735E-16,1.,0.));
#23950=DIRECTION('ref_axis',(1.,-1.22464679914735E-16,0.));
#23951=DIRECTION('center_axis',(0.,0.,-1.));
#23952=DIRECTION('ref_axis',(-1.,0.,0.));
#23953=DIRECTION('center_axis',(0.,0.,-1.));
#23954=DIRECTION('ref_axis',(-1.,0.,0.));
#23955=DIRECTION('',(0.777743299254267,-9.5246084199004E-17,-0.628582023657285));
#23956=DIRECTION('center_axis',(0.,0.,-1.));
#23957=DIRECTION('ref_axis',(-1.,0.,0.));
#23958=DIRECTION('center_axis',(-1.22464679914735E-16,-1.,0.));
#23959=DIRECTION('ref_axis',(1.,-1.22464679914735E-16,0.));
#23960=DIRECTION('center_axis',(0.,0.,1.));
#23961=DIRECTION('ref_axis',(3.28564782949089E-13,1.,0.));
#23962=DIRECTION('center_axis',(6.13527734841807E-15,-1.,1.38135285440519E-14));
#23963=DIRECTION('ref_axis',(0.342009281678287,1.50733243649404E-14,0.939696574031162));
#23964=DIRECTION('center_axis',(0.,0.,-1.));
#23965=DIRECTION('ref_axis',(-1.,0.,0.));
#23966=DIRECTION('center_axis',(0.707106781186538,0.707106781186557,-2.18052895483717E-14));
#23967=DIRECTION('ref_axis',(0.668377159293621,-0.668377159293593,0.326410701217372));
#23968=DIRECTION('center_axis',(0.,0.,1.));
#23969=DIRECTION('ref_axis',(0.707106781186608,0.707106781186487,0.));
#23970=DIRECTION('center_axis',(-0.707106781186536,-0.707106781186559,1.97361719728453E-14));
#23971=DIRECTION('ref_axis',(0.241837082303476,-0.241837082303441,0.939696574031161));
#23972=DIRECTION('center_axis',(0.,0.,-1.));
#23973=DIRECTION('ref_axis',(-1.,0.,0.));
#23974=DIRECTION('center_axis',(1.,7.91804511680167E-15,-7.69942093215295E-15));
#23975=DIRECTION('ref_axis',(1.00035767704373E-14,-0.945228043453423,0.326410701217368));
#23976=DIRECTION('center_axis',(0.,0.,1.));
#23977=DIRECTION('ref_axis',(1.,-8.08242361927114E-14,0.));
#23978=DIRECTION('center_axis',(-1.,-1.79398764678015E-15,1.76453926386396E-15));
#23979=DIRECTION('ref_axis',(2.26983333538778E-15,-0.342009281678289,0.939696574031161));
#23980=DIRECTION('center_axis',(0.,0.,-1.));
#23981=DIRECTION('ref_axis',(-1.,0.,0.));
#23982=DIRECTION('center_axis',(0.707106781186538,-0.707106781186557,4.77488092300106E-15));
#23983=DIRECTION('ref_axis',(-0.668377159293619,-0.6683771592936,0.326410701217363));
#23984=DIRECTION('center_axis',(0.,0.,1.));
#23985=DIRECTION('ref_axis',(0.707106781186484,-0.707106781186611,0.));
#23986=DIRECTION('center_axis',(-0.707106781186529,0.707106781186566,-1.90995212640436E-14));
#23987=DIRECTION('ref_axis',(-0.241837082303473,-0.241837082303435,0.939696574031163));
#23988=DIRECTION('center_axis',(0.,0.,-1.));
#23989=DIRECTION('ref_axis',(-1.,0.,0.));
#23990=DIRECTION('center_axis',(-1.02700574112875E-14,-1.,-4.88525407613946E-17));
#23991=DIRECTION('ref_axis',(-0.945228043453422,9.69096499636107E-15,0.326410701217372));
#23992=DIRECTION('center_axis',(0.,0.,1.));
#23993=DIRECTION('ref_axis',(3.13710679174016E-13,-1.,0.));
#23994=DIRECTION('center_axis',(1.0700730164861E-14,1.,-6.44787115032575E-17));
#23995=DIRECTION('ref_axis',(-0.342009281678279,3.72415768800159E-15,0.939696574031164));
#23996=DIRECTION('center_axis',(0.,0.,-1.));
#23997=DIRECTION('ref_axis',(-1.,0.,0.));
#23998=DIRECTION('center_axis',(-0.707106781186564,-0.707106781186531,1.16188769126359E-14));
#23999=DIRECTION('ref_axis',(-0.66837715929359,0.668377159293628,0.326410701217364));
#24000=DIRECTION('center_axis',(0.,0.,1.));
#24001=DIRECTION('ref_axis',(-0.707106781186613,-0.707106781186482,0.));
#24002=DIRECTION('center_axis',(0.707106781186545,0.70710678118655,1.49612916568344E-14));
#24003=DIRECTION('ref_axis',(-0.24183708230347,0.241837082303447,0.939696574031161));
#24004=DIRECTION('center_axis',(0.,0.,-1.));
#24005=DIRECTION('ref_axis',(-1.,0.,0.));
#24006=DIRECTION('center_axis',(-1.,1.15612551933786E-14,1.13714767015716E-14));
#24007=DIRECTION('ref_axis',(1.46383861165231E-14,0.945228043453423,0.326410701217368));
#24008=DIRECTION('center_axis',(0.,0.,1.));
#24009=DIRECTION('ref_axis',(-1.,8.08242361927114E-14,0.));
#24010=DIRECTION('center_axis',(1.,1.65009199484293E-15,1.71165480509254E-15));
#24011=DIRECTION('ref_axis',(-2.1746906207308E-15,0.342009281678289,0.939696574031161));
#24012=DIRECTION('center_axis',(0.,0.,-1.));
#24013=DIRECTION('ref_axis',(-1.,0.,0.));
#24014=DIRECTION('center_axis',(-0.707106781186527,0.707106781186568,2.46702181021724E-14));
#24015=DIRECTION('ref_axis',(0.668377159293632,0.668377159293584,0.326410701217368));
#24016=DIRECTION('center_axis',(0.,0.,1.));
#24017=DIRECTION('ref_axis',(-0.707106781186489,0.707106781186606,0.));
#24018=DIRECTION('center_axis',(0.707106781186532,-0.707106781186563,-1.36879902392314E-14));
#24019=DIRECTION('ref_axis',(0.241837082303472,0.241837082303443,0.939696574031161));
#24020=DIRECTION('center_axis',(0.,0.,-1.));
#24021=DIRECTION('ref_axis',(-1.,0.,0.));
#24022=DIRECTION('center_axis',(2.65449697024962E-14,1.,1.84854068675772E-14));
#24023=DIRECTION('ref_axis',(0.945228043453424,-3.1125259244975E-14,0.326410701217364));
#24024=DIRECTION('center_axis',(0.,0.,1.));
#24025=DIRECTION('ref_axis',(3.28564782949089E-13,1.,0.));
#24026=DIRECTION('center_axis',(0.,0.,-1.));
#24027=DIRECTION('ref_axis',(-1.,0.,0.));
#24028=DIRECTION('',(-0.93969517819209,3.34165038880862E-15,0.342013116828193));
#24029=DIRECTION('center_axis',(0.,0.,-1.));
#24030=DIRECTION('ref_axis',(-1.,0.,0.));
#24031=DIRECTION('',(0.664464832747924,-0.664464832747934,-0.34201311682819));
#24032=DIRECTION('center_axis',(0.,0.,-1.));
#24033=DIRECTION('ref_axis',(-1.,0.,0.));
#24034=DIRECTION('center_axis',(0.,0.,-1.));
#24035=DIRECTION('ref_axis',(-1.,0.,0.));
#24036=DIRECTION('',(0.93969517819209,-3.2601467207889E-15,-0.342013116828193));
#24037=DIRECTION('',(-0.664464832747918,-0.664464832747939,0.342013116828193));
#24038=DIRECTION('center_axis',(0.,0.,-1.));
#24039=DIRECTION('ref_axis',(-1.,0.,0.));
#24040=DIRECTION('',(-0.664464832747928,0.664464832747928,0.342013116828193));
#24041=DIRECTION('center_axis',(0.,0.,-1.));
#24042=DIRECTION('ref_axis',(-1.,0.,0.));
#24043=DIRECTION('',(8.15036680197226E-17,-0.93969517819209,-0.342013116828193));
#24044=DIRECTION('center_axis',(0.,0.,-1.));
#24045=DIRECTION('ref_axis',(-1.,0.,0.));
#24046=DIRECTION('',(8.15036680197226E-17,0.93969517819209,0.342013116828193));
#24047=DIRECTION('center_axis',(0.,0.,-1.));
#24048=DIRECTION('ref_axis',(-1.,0.,0.));
#24049=DIRECTION('',(-0.66446483274794,-0.664464832747919,-0.342013116828188));
#24050=DIRECTION('center_axis',(0.,0.,-1.));
#24051=DIRECTION('ref_axis',(-1.,0.,0.));
#24052=DIRECTION('',(0.664464832747934,0.664464832747924,0.34201311682819));
#24053=DIRECTION('center_axis',(0.,0.,-1.));
#24054=DIRECTION('ref_axis',(-1.,0.,0.));
#24055=DIRECTION('',(-0.93969517819209,9.78044016236671E-15,-0.342013116828193));
#24056=DIRECTION('center_axis',(0.,0.,-1.));
#24057=DIRECTION('ref_axis',(-1.,0.,0.));
#24058=DIRECTION('',(0.939695178192092,-9.94344749840606E-15,0.34201311682819));
#24059=DIRECTION('center_axis',(0.,0.,-1.));
#24060=DIRECTION('ref_axis',(-1.,0.,0.));
#24061=DIRECTION('',(-0.664464832747918,0.664464832747939,-0.342013116828193));
#24062=DIRECTION('center_axis',(0.,0.,-1.));
#24063=DIRECTION('ref_axis',(-1.,0.,0.));
#24064=DIRECTION('',(0.664464832747918,-0.664464832747939,0.342013116828193));
#24065=DIRECTION('center_axis',(0.,0.,-1.));
#24066=DIRECTION('ref_axis',(-1.,0.,0.));
#24067=DIRECTION('',(-8.15036680197226E-17,0.93969517819209,-0.342013116828193));
#24068=DIRECTION('center_axis',(0.,0.,-1.));
#24069=DIRECTION('ref_axis',(-1.,0.,0.));
#24070=DIRECTION('center_axis',(0.,0.,-1.));
#24071=DIRECTION('ref_axis',(-1.,0.,0.));
#24072=DIRECTION('',(0.664464832747934,0.664464832747924,-0.34201311682819));
#24073=DIRECTION('',(-8.15036680197226E-17,-0.93969517819209,0.342013116828193));
#24074=DIRECTION('center_axis',(0.,0.,1.));
#24075=DIRECTION('ref_axis',(1.,0.,0.));
#24076=DIRECTION('',(-0.342027306942117,1.29765967489722E-15,-0.939690013411829));
#24077=DIRECTION('center_axis',(0.,0.,-1.));
#24078=DIRECTION('ref_axis',(-1.,0.,0.));
#24079=DIRECTION('',(0.241849828089742,-0.241849828089742,0.939690013411829));
#24080=DIRECTION('center_axis',(0.,0.,1.));
#24081=DIRECTION('ref_axis',(1.,0.,0.));
#24082=DIRECTION('center_axis',(0.,0.,-1.));
#24083=DIRECTION('ref_axis',(-1.,0.,0.));
#24084=DIRECTION('',(0.342027306942117,-1.08138306241435E-15,0.939690013411829));
#24085=DIRECTION('',(-0.241849828089751,-0.241849828089742,-0.939690013411827));
#24086=DIRECTION('center_axis',(0.,0.,1.));
#24087=DIRECTION('ref_axis',(1.,0.,0.));
#24088=DIRECTION('',(-0.241849828089734,0.241849828089743,-0.939690013411832));
#24089=DIRECTION('center_axis',(0.,0.,-1.));
#24090=DIRECTION('ref_axis',(-1.,0.,0.));
#24091=DIRECTION('',(7.20922041609565E-17,-0.342027306942117,0.939690013411829));
#24092=DIRECTION('center_axis',(0.,0.,1.));
#24093=DIRECTION('ref_axis',(1.,0.,0.));
#24094=DIRECTION('',(7.20922041609565E-17,0.342027306942117,-0.939690013411829));
#24095=DIRECTION('center_axis',(0.,0.,-1.));
#24096=DIRECTION('ref_axis',(-1.,0.,0.));
#24097=DIRECTION('',(-0.241849828089734,-0.241849828089743,0.939690013411832));
#24098=DIRECTION('center_axis',(0.,0.,1.));
#24099=DIRECTION('ref_axis',(1.,0.,0.));
#24100=DIRECTION('',(0.241849828089751,0.241849828089742,-0.939690013411827));
#24101=DIRECTION('center_axis',(0.,0.,-1.));
#24102=DIRECTION('ref_axis',(-1.,0.,0.));
#24103=DIRECTION('',(-0.342027306942125,3.4604257997259E-15,0.939690013411826));
#24104=DIRECTION('center_axis',(0.,0.,1.));
#24105=DIRECTION('ref_axis',(1.,0.,0.));
#24106=DIRECTION('',(0.342027306942117,-3.74879461636974E-15,-0.939690013411829));
#24107=DIRECTION('center_axis',(0.,0.,-1.));
#24108=DIRECTION('ref_axis',(-1.,0.,0.));
#24109=DIRECTION('',(-0.241849828089742,0.241849828089751,0.939690013411827));
#24110=DIRECTION('center_axis',(0.,0.,1.));
#24111=DIRECTION('ref_axis',(1.,0.,0.));
#24112=DIRECTION('',(0.241849828089733,-0.241849828089752,-0.939690013411829));
#24113=DIRECTION('center_axis',(0.,0.,-1.));
#24114=DIRECTION('ref_axis',(-1.,0.,0.));
#24115=DIRECTION('',(-7.20922041609565E-17,0.342027306942117,0.939690013411829));
#24116=DIRECTION('center_axis',(0.,0.,1.));
#24117=DIRECTION('ref_axis',(1.,0.,0.));
#24118=DIRECTION('center_axis',(0.,0.,-1.));
#24119=DIRECTION('ref_axis',(-1.,0.,0.));
#24120=DIRECTION('',(0.241849828089734,0.241849828089743,0.939690013411832));
#24121=DIRECTION('',(-7.20922041609565E-17,-0.342027306942117,-0.939690013411829));
#24122=DIRECTION('center_axis',(0.,0.,-1.));
#24123=DIRECTION('ref_axis',(-1.,0.,0.));
#24124=DIRECTION('',(0.573585346078431,-2.07701987415471E-15,-0.819145805558501));
#24125=DIRECTION('',(-0.405586087801291,0.405586087801293,0.819145805558501));
#24126=DIRECTION('center_axis',(0.,0.,-1.));
#24127=DIRECTION('ref_axis',(-1.,0.,0.));
#24128=DIRECTION('',(-0.573585346078431,1.91898575329511E-15,0.819145805558501));
#24129=DIRECTION('',(0.405586087801295,0.405586087801293,-0.819145805558499));
#24130=DIRECTION('center_axis',(0.,0.,-1.));
#24131=DIRECTION('ref_axis',(-1.,0.,0.));
#24132=DIRECTION('',(0.405586087801291,-0.405586087801293,-0.819145805558501));
#24133=DIRECTION('',(-6.77289089398275E-17,0.573585346078431,0.819145805558501));
#24134=DIRECTION('center_axis',(0.,0.,-1.));
#24135=DIRECTION('ref_axis',(-1.,0.,0.));
#24136=DIRECTION('',(-9.030521191977E-17,-0.573585346078431,-0.819145805558501));
#24137=DIRECTION('',(0.405586087801294,0.405586087801288,0.819145805558502));
#24138=DIRECTION('center_axis',(0.,0.,-1.));
#24139=DIRECTION('ref_axis',(-1.,0.,0.));
#24140=DIRECTION('',(-0.405586087801298,-0.40558608780129,-0.819145805558499));
#24141=DIRECTION('',(0.573585346078431,-5.93756768372488E-15,0.819145805558501));
#24142=DIRECTION('center_axis',(0.,0.,-1.));
#24143=DIRECTION('ref_axis',(-1.,0.,0.));
#24144=DIRECTION('',(-0.573585346078433,6.11817810756441E-15,-0.8191458055585));
#24145=DIRECTION('',(0.405586087801288,-0.405586087801296,0.819145805558501));
#24146=DIRECTION('center_axis',(0.,0.,-1.));
#24147=DIRECTION('ref_axis',(-1.,0.,0.));
#24148=DIRECTION('',(-0.405586087801287,0.405586087801299,-0.8191458055585));
#24149=DIRECTION('',(6.77289089398275E-17,-0.573585346078431,0.819145805558501));
#24150=DIRECTION('center_axis',(0.,0.,-1.));
#24151=DIRECTION('ref_axis',(-1.,0.,0.));
#24152=DIRECTION('',(-0.405586087801294,-0.405586087801288,0.819145805558502));
#24153=DIRECTION('',(9.030521191977E-17,0.573585346078431,-0.819145805558501));
#24154=DIRECTION('center_axis',(0.,0.,1.));
#24155=DIRECTION('ref_axis',(1.,0.,0.));
#24156=DIRECTION('center_axis',(0.,0.,-1.));
#24157=DIRECTION('ref_axis',(-1.,0.,0.));
#24158=DIRECTION('center_axis',(-1.,1.27191845719472E-16,0.));
#24159=DIRECTION('ref_axis',(-1.27191845719472E-16,-1.,0.));
#24160=DIRECTION('',(1.27191845719472E-16,1.,0.));
#24161=DIRECTION('center_axis',(1.,1.27191845719472E-16,0.));
#24162=DIRECTION('ref_axis',(-1.27191845719472E-16,1.,0.));
#24163=DIRECTION('',(1.27191845719472E-16,-1.,0.));
#24164=DIRECTION('center_axis',(0.,0.,-1.));
#24165=DIRECTION('ref_axis',(-1.,0.,0.));
#24166=DIRECTION('center_axis',(-0.707106781186546,0.707106781186549,0.));
#24167=DIRECTION('ref_axis',(-0.707106781186549,-0.707106781186546,0.));
#24168=DIRECTION('',(0.707106781186549,0.707106781186546,0.));
#24169=DIRECTION('center_axis',(0.707106781186546,-0.707106781186549,0.));
#24170=DIRECTION('ref_axis',(0.707106781186549,0.707106781186546,0.));
#24171=DIRECTION('',(-0.707106781186549,-0.707106781186546,0.));
#24172=DIRECTION('center_axis',(0.,0.,-1.));
#24173=DIRECTION('ref_axis',(-0.707106781186546,0.707106781186549,0.));
#24174=DIRECTION('center_axis',(-0.707106781186556,-0.707106781186539,0.));
#24175=DIRECTION('ref_axis',(0.707106781186539,-0.707106781186556,0.));
#24176=DIRECTION('',(-0.707106781186539,0.707106781186556,0.));
#24177=DIRECTION('center_axis',(0.707106781186556,0.707106781186539,0.));
#24178=DIRECTION('ref_axis',(-0.707106781186539,0.707106781186556,0.));
#24179=DIRECTION('',(0.707106781186539,-0.707106781186556,0.));
#24180=DIRECTION('center_axis',(0.,0.,-1.));
#24181=DIRECTION('ref_axis',(-0.707106781186556,-0.707106781186539,0.));
#24182=DIRECTION('center_axis',(-1.06016358622489E-14,-1.,0.));
#24183=DIRECTION('ref_axis',(1.,-1.06016358622489E-14,0.));
#24184=DIRECTION('',(-1.,1.06016358622489E-14,0.));
#24185=DIRECTION('center_axis',(1.03472521708099E-14,1.,0.));
#24186=DIRECTION('ref_axis',(-1.,1.03472521708099E-14,0.));
#24187=DIRECTION('',(1.,-1.03472521708099E-14,0.));
#24188=DIRECTION('center_axis',(0.,0.,-1.));
#24189=DIRECTION('ref_axis',(-1.04744440165294E-14,-1.,0.));
#24190=DIRECTION('center_axis',(0.707106781186541,-0.707106781186554,0.));
#24191=DIRECTION('ref_axis',(0.707106781186554,0.707106781186541,0.));
#24192=DIRECTION('',(-0.707106781186554,-0.707106781186541,0.));
#24193=DIRECTION('center_axis',(-0.707106781186541,0.707106781186554,0.));
#24194=DIRECTION('ref_axis',(-0.707106781186554,-0.707106781186541,0.));
#24195=DIRECTION('',(0.707106781186554,0.707106781186541,0.));
#24196=DIRECTION('center_axis',(0.,0.,-1.));
#24197=DIRECTION('ref_axis',(0.707106781186541,-0.707106781186554,0.));
#24198=DIRECTION('center_axis',(1.,-1.27191845719472E-16,0.));
#24199=DIRECTION('ref_axis',(1.27191845719472E-16,1.,0.));
#24200=DIRECTION('',(-1.27191845719472E-16,-1.,0.));
#24201=DIRECTION('center_axis',(-1.,-1.27191845719472E-16,0.));
#24202=DIRECTION('ref_axis',(1.27191845719472E-16,-1.,0.));
#24203=DIRECTION('',(-1.27191845719472E-16,1.,0.));
#24204=DIRECTION('center_axis',(0.,0.,-1.));
#24205=DIRECTION('ref_axis',(1.,0.,0.));
#24206=DIRECTION('center_axis',(0.707106781186551,0.707106781186544,0.));
#24207=DIRECTION('ref_axis',(-0.707106781186544,0.707106781186551,0.));
#24208=DIRECTION('',(0.707106781186544,-0.707106781186551,0.));
#24209=DIRECTION('center_axis',(-0.707106781186551,-0.707106781186544,0.));
#24210=DIRECTION('ref_axis',(0.707106781186544,-0.707106781186551,0.));
#24211=DIRECTION('',(-0.707106781186544,0.707106781186551,0.));
#24212=DIRECTION('center_axis',(0.,0.,-1.));
#24213=DIRECTION('ref_axis',(0.707106781186551,0.707106781186544,0.));
#24214=DIRECTION('center_axis',(3.61867318456261E-15,1.,0.));
#24215=DIRECTION('ref_axis',(-1.,3.61867318456261E-15,0.));
#24216=DIRECTION('',(1.,-3.61867318456261E-15,0.));
#24217=DIRECTION('center_axis',(-3.36428949312366E-15,-1.,0.));
#24218=DIRECTION('ref_axis',(1.,-3.36428949312366E-15,0.));
#24219=DIRECTION('',(-1.,3.36428949312366E-15,0.));
#24220=DIRECTION('center_axis',(0.,0.,-1.));
#24221=DIRECTION('ref_axis',(3.49148133884313E-15,1.,0.));
#28602=CARTESIAN_POINT('',(0.,0.,0.));
#28603=CARTESIAN_POINT('Origin',(0.,0.,0.));
#28604=CARTESIAN_POINT('',(8.671875,1.0619983961356E-15,-5.39));
#28605=CARTESIAN_POINT('Origin',(0.,0.,-5.39));
#28606=CARTESIAN_POINT('',(8.671875,1.0619983961356E-15,-4.95));
#28607=CARTESIAN_POINT('',(8.671875,1.0619983961356E-15,0.));
#28608=CARTESIAN_POINT('Origin',(0.,0.,-4.95));
#28609=CARTESIAN_POINT('Origin',(0.,0.,-5.39));
#28610=CARTESIAN_POINT('',(8.781875,1.07546951092622E-15,-5.5));
#28611=CARTESIAN_POINT('Origin',(0.,0.,-5.5));
#28612=CARTESIAN_POINT('Origin',(8.781875,1.07546951092622E-15,-5.39));
#28613=CARTESIAN_POINT('Origin',(0.,0.,-0.10725138426002));
#28614=CARTESIAN_POINT('',(13.0772848379569,1.60150550183421E-15,-4.30142548471451));
#28615=CARTESIAN_POINT('Origin',(0.,0.,-4.30142548471451));
#28616=CARTESIAN_POINT('',(9.6875,1.186376586674E-15,-5.5));
#28617=CARTESIAN_POINT('Origin',(9.6875,1.186376586674E-15,-0.10725138426002));
#28618=CARTESIAN_POINT('Origin',(0.,0.,-5.5));
#28619=CARTESIAN_POINT('Origin',(0.,0.,-3.66302186693758));
#28620=CARTESIAN_POINT('',(13.867180376262,1.69823980609882E-15,-3.66302186693758));
#28621=CARTESIAN_POINT('Origin',(0.,0.,-3.66302186693758));
#28622=CARTESIAN_POINT('',(13.867180376262,1.69823980609882E-15,-3.66302186693758));
#28623=CARTESIAN_POINT('Origin',(0.,0.,-4.22788751277274));
#28624=CARTESIAN_POINT('',(-14.9183171404923,-0.0999999999998437,-4.64446921070048));
#28625=CARTESIAN_POINT('',(-14.9183171404923,0.100000000000156,-4.64446921070048));
#28626=CARTESIAN_POINT('Origin',(0.,0.,-4.64446921070048));
#28627=CARTESIAN_POINT('',(-10.6195538920522,10.4781325358151,-4.64446921070048));
#28628=CARTESIAN_POINT('Origin',(0.,0.,-4.64446921070048));
#28629=CARTESIAN_POINT('',(-10.4781325358149,10.6195538920524,-4.64446921070048));
#28630=CARTESIAN_POINT('Origin',(0.,0.,-4.64446921070048));
#28631=CARTESIAN_POINT('',(-0.0999999999999999,14.9183171404923,-4.64446921070048));
#28632=CARTESIAN_POINT('Origin',(0.,0.,-4.64446921070048));
#28633=CARTESIAN_POINT('',(0.0999999999999999,14.9183171404923,-4.64446921070048));
#28634=CARTESIAN_POINT('Origin',(0.,0.,-4.64446921070048));
#28635=CARTESIAN_POINT('',(10.478132535815,10.6195538920523,-4.64446921070048));
#28636=CARTESIAN_POINT('Origin',(0.,0.,-4.64446921070048));
#28637=CARTESIAN_POINT('',(10.6195538920523,10.478132535815,-4.64446921070048));
#28638=CARTESIAN_POINT('Origin',(0.,0.,-4.64446921070048));
#28639=CARTESIAN_POINT('',(14.9183171404923,0.0999999999999478,-4.64446921070048));
#28640=CARTESIAN_POINT('Origin',(0.,0.,-4.64446921070048));
#28641=CARTESIAN_POINT('',(14.9186522951742,1.82700797808774E-15,-4.64446921070048));
#28642=CARTESIAN_POINT('Origin',(0.,0.,-4.64446921070048));
#28643=CARTESIAN_POINT('Origin',(14.3237119736335,1.75414880204189E-15,
-4.22788751277274));
#28644=CARTESIAN_POINT('',(14.9183171404923,-0.100000000000052,-4.64446921070048));
#28645=CARTESIAN_POINT('Origin',(0.,0.,-4.64446921070048));
#28646=CARTESIAN_POINT('',(10.6195538920522,-10.478132535815,-4.64446921070048));
#28647=CARTESIAN_POINT('Origin',(0.,0.,-4.64446921070048));
#28648=CARTESIAN_POINT('',(10.4781325358149,-10.6195538920523,-4.64446921070048));
#28649=CARTESIAN_POINT('Origin',(0.,0.,-4.64446921070048));
#28650=CARTESIAN_POINT('',(0.0999999999999999,-14.9183171404923,-4.64446921070048));
#28651=CARTESIAN_POINT('Origin',(0.,0.,-4.64446921070048));
#28652=CARTESIAN_POINT('',(-0.0999999999999999,-14.9183171404923,-4.64446921070048));
#28653=CARTESIAN_POINT('Origin',(0.,0.,-4.64446921070048));
#28654=CARTESIAN_POINT('',(-10.4781325358151,-10.6195538920522,-4.64446921070048));
#28655=CARTESIAN_POINT('Origin',(0.,0.,-4.64446921070048));
#28656=CARTESIAN_POINT('',(-10.6195538920524,-10.4781325358149,-4.64446921070048));
#28657=CARTESIAN_POINT('Origin',(0.,0.,-4.64446921070048));
#28658=CARTESIAN_POINT('Origin',(0.,0.,-4.64446921070048));
#28659=CARTESIAN_POINT('Origin',(0.,0.,-3.87366667012467));
#28660=CARTESIAN_POINT('',(12.7315647249454,1.55916699885417E-15,-3.87366667012467));
#28661=CARTESIAN_POINT('Origin',(0.,0.,-3.87366667012467));
#28662=CARTESIAN_POINT('',(13.5214602632505,1.65590130311878E-15,-3.23526305234773));
#28663=CARTESIAN_POINT('',(12.7315647249454,1.55916699885417E-15,-3.87366667012467));
#28664=CARTESIAN_POINT('Origin',(0.,0.,-3.23526305234774));
#28665=CARTESIAN_POINT('Origin',(0.,0.,-0.10725138426002));
#28666=CARTESIAN_POINT('',(9.6875,1.186376586674E-15,-4.95));
#28667=CARTESIAN_POINT('Origin',(0.,0.,-4.95));
#28668=CARTESIAN_POINT('Origin',(9.6875,1.186376586674E-15,-0.10725138426002));
#28669=CARTESIAN_POINT('Origin',(0.,0.,-4.22788751277274));
#28670=CARTESIAN_POINT('',(15.5300994798678,1.901888661846E-15,-4.64446921070048));
#28671=CARTESIAN_POINT('Origin',(14.3237119736335,1.75414880204189E-15,
-4.22788751277274));
#28672=CARTESIAN_POINT('',(15.5297775210912,0.0999999999999458,-4.64446921070048));
#28673=CARTESIAN_POINT('Origin',(0.,0.,-4.64446921070048));
#28674=CARTESIAN_POINT('',(14.7598894352984,0.0999999999999484,-5.42720595314676));
#28675=CARTESIAN_POINT('Origin',(14.3233829927518,0.0999999999999847,-4.22787124085886));
#28676=CARTESIAN_POINT('',(10.5075285873819,10.3661072311445,-5.42720595314676));
#28677=CARTESIAN_POINT('Origin',(0.,0.,-5.42720595314676));
#28678=CARTESIAN_POINT('',(11.0519216736007,10.9105003173633,-4.64446921070048));
#28679=CARTESIAN_POINT('Origin',(10.1988719278759,10.0574505716386,-4.22787124927498));
#28680=CARTESIAN_POINT('',(10.9105003173634,11.0519216736006,-4.64446921070048));
#28681=CARTESIAN_POINT('Origin',(0.,0.,-4.64446921070048));
#28682=CARTESIAN_POINT('',(10.3661072311446,10.5075285873818,-5.42720595314676));
#28683=CARTESIAN_POINT('Origin',(10.0574505655882,10.1988719218255,-4.22787124085886));
#28684=CARTESIAN_POINT('',(0.0999999999999999,14.7598894352984,-5.42720595314676));
#28685=CARTESIAN_POINT('Origin',(0.,0.,-5.42720595314676));
#28686=CARTESIAN_POINT('',(0.1,15.5297775210912,-4.64446921070048));
#28687=CARTESIAN_POINT('Origin',(0.100000000000003,14.3233830013084,-4.22787124927497));
#28688=CARTESIAN_POINT('',(-0.1,15.5297775210912,-4.64446921070048));
#28689=CARTESIAN_POINT('Origin',(0.,0.,-4.64446921070048));
#28690=CARTESIAN_POINT('',(-0.0999999999999999,14.7598894352984,-5.42720595314676));
#28691=CARTESIAN_POINT('Origin',(-0.100000000000018,14.3233829927518,-4.22787124085886));
#28692=CARTESIAN_POINT('',(-10.3661072311444,10.507528587382,-5.42720595314676));
#28693=CARTESIAN_POINT('Origin',(0.,0.,-5.42720595314676));
#28694=CARTESIAN_POINT('',(-10.9105003173632,11.0519216736008,-4.64446921070048));
#28695=CARTESIAN_POINT('Origin',(-10.0574505716385,10.1988719278761,-4.22787124927498));
#28696=CARTESIAN_POINT('',(-11.0519216736005,10.9105003173635,-4.64446921070048));
#28697=CARTESIAN_POINT('Origin',(0.,0.,-4.64446921070048));
#28698=CARTESIAN_POINT('',(-10.5075285873817,10.3661072311447,-5.42720595314676));
#28699=CARTESIAN_POINT('Origin',(-10.1988719218254,10.0574505655883,-4.22787124085886));
#28700=CARTESIAN_POINT('',(-14.7598894352984,0.100000000000155,-5.42720595314676));
#28701=CARTESIAN_POINT('Origin',(0.,0.,-5.42720595314676));
#28702=CARTESIAN_POINT('',(-15.5297775210912,0.100000000000163,-4.64446921070048));
#28703=CARTESIAN_POINT('Origin',(-14.3233830013084,0.10000000000015,-4.227871249275));
#28704=CARTESIAN_POINT('',(-15.5297775210912,-0.0999999999998373,-4.64446921070048));
#28705=CARTESIAN_POINT('Origin',(0.,0.,-4.64446921070048));
#28706=CARTESIAN_POINT('',(-14.7598894352984,-0.0999999999998453,-5.42720595314676));
#28707=CARTESIAN_POINT('Origin',(-14.3233829927518,-0.0999999999998497,
-4.22787124085885));
#28708=CARTESIAN_POINT('',(-10.5075285873819,-10.3661072311445,-5.42720595314676));
#28709=CARTESIAN_POINT('Origin',(0.,0.,-5.42720595314676));
#28710=CARTESIAN_POINT('',(-11.0519216736007,-10.9105003173632,-4.64446921070048));
#28711=CARTESIAN_POINT('Origin',(-10.198871927876,-10.0574505716385,-4.22787124927499));
#28712=CARTESIAN_POINT('',(-10.9105003173634,-11.0519216736006,-4.64446921070048));
#28713=CARTESIAN_POINT('Origin',(0.,0.,-4.64446921070048));
#28714=CARTESIAN_POINT('',(-10.3661072311446,-10.5075285873818,-5.42720595314676));
#28715=CARTESIAN_POINT('Origin',(-10.0574505655883,-10.1988719218254,-4.22787124085886));
#28716=CARTESIAN_POINT('',(-0.0999999999999999,-14.7598894352984,-5.42720595314676));
#28717=CARTESIAN_POINT('Origin',(0.,0.,-5.42720595314676));
#28718=CARTESIAN_POINT('',(-0.1,-15.5297775210912,-4.64446921070048));
#28719=CARTESIAN_POINT('Origin',(-0.100000000000002,-14.3233830013084,-4.22787124927497));
#28720=CARTESIAN_POINT('',(0.1,-15.5297775210912,-4.64446921070048));
#28721=CARTESIAN_POINT('Origin',(0.,0.,-4.64446921070048));
#28722=CARTESIAN_POINT('',(0.0999999999999999,-14.7598894352984,-5.42720595314676));
#28723=CARTESIAN_POINT('Origin',(0.099999999999988,-14.3233829927518,-4.22787124085886));
#28724=CARTESIAN_POINT('',(10.3661072311445,-10.5075285873819,-5.42720595314676));
#28725=CARTESIAN_POINT('Origin',(0.,0.,-5.42720595314676));
#28726=CARTESIAN_POINT('',(10.9105003173633,-11.0519216736007,-4.64446921070048));
#28727=CARTESIAN_POINT('Origin',(10.0574505716385,-10.198871927876,-4.22787124927498));
#28728=CARTESIAN_POINT('',(11.0519216736006,-10.9105003173634,-4.64446921070048));
#28729=CARTESIAN_POINT('Origin',(0.,0.,-4.64446921070048));
#28730=CARTESIAN_POINT('',(10.5075285873818,-10.3661072311446,-5.42720595314676));
#28731=CARTESIAN_POINT('Origin',(10.1988719218254,-10.0574505655883,-4.22787124085885));
#28732=CARTESIAN_POINT('',(14.7598894352984,-0.100000000000051,-5.42720595314676));
#28733=CARTESIAN_POINT('Origin',(0.,0.,-5.42720595314676));
#28734=CARTESIAN_POINT('',(15.5297775210912,-0.100000000000054,-4.64446921070048));
#28735=CARTESIAN_POINT('Origin',(14.3233830013084,-0.100000000000069,-4.22787124927498));
#28736=CARTESIAN_POINT('Origin',(0.,0.,-4.64446921070048));
#28737=CARTESIAN_POINT('Origin',(0.,0.,-5.42720595314676));
#28738=CARTESIAN_POINT('',(10.3661039408187,-10.2246825845815,-5.5));
#28739=CARTESIAN_POINT('',(10.3661039408187,-10.2246825845815,-5.5));
#28740=CARTESIAN_POINT('',(14.559884782075,-0.100000000000051,-5.5));
#28741=CARTESIAN_POINT('Origin',(0.,0.,-5.5));
#28742=CARTESIAN_POINT('',(14.7598894352984,-0.100000000000051,-5.42720595314676));
#28743=CARTESIAN_POINT('Origin',(0.,0.,-5.42720595314676));
#28744=CARTESIAN_POINT('',(10.3661039408187,10.2246825845814,-5.5));
#28745=CARTESIAN_POINT('',(14.559884782075,0.099999999999949,-5.5));
#28746=CARTESIAN_POINT('Origin',(0.,0.,-5.5));
#28747=CARTESIAN_POINT('',(10.5075285873819,10.3661072311445,-5.42720595314676));
#28748=CARTESIAN_POINT('',(14.559884782075,0.099999999999949,-5.5));
#28749=CARTESIAN_POINT('Origin',(0.,0.,-5.42720595314676));
#28750=CARTESIAN_POINT('',(0.0999999999999999,-14.559884782075,-5.5));
#28751=CARTESIAN_POINT('',(0.0999999999999999,-14.559884782075,-5.5));
#28752=CARTESIAN_POINT('',(10.2246825845814,-10.3661039408188,-5.5));
#28753=CARTESIAN_POINT('Origin',(0.,0.,-5.5));
#28754=CARTESIAN_POINT('',(10.3661072311445,-10.5075285873819,-5.42720595314676));
#28755=CARTESIAN_POINT('Origin',(0.,0.,-5.42720595314676));
#28756=CARTESIAN_POINT('',(-10.2246825845815,-10.3661039408186,-5.5));
#28757=CARTESIAN_POINT('',(-10.2246825845815,-10.3661039408186,-5.5));
#28758=CARTESIAN_POINT('',(-0.0999999999999999,-14.559884782075,-5.5));
#28759=CARTESIAN_POINT('Origin',(0.,0.,-5.5));
#28760=CARTESIAN_POINT('',(-0.0999999999999999,-14.7598894352984,-5.42720595314676));
#28761=CARTESIAN_POINT('Origin',(0.,0.,-5.42720595314676));
#28762=CARTESIAN_POINT('',(-14.559884782075,-0.0999999999998474,-5.5));
#28763=CARTESIAN_POINT('',(-14.559884782075,-0.0999999999998474,-5.5));
#28764=CARTESIAN_POINT('',(-10.3661039408188,-10.2246825845813,-5.5));
#28765=CARTESIAN_POINT('Origin',(0.,0.,-5.5));
#28766=CARTESIAN_POINT('',(-10.5075285873819,-10.3661072311445,-5.42720595314676));
#28767=CARTESIAN_POINT('Origin',(0.,0.,-5.42720595314676));
#28768=CARTESIAN_POINT('',(-10.3661039408186,10.2246825845815,-5.5));
#28769=CARTESIAN_POINT('',(-10.3661039408186,10.2246825845815,-5.5));
#28770=CARTESIAN_POINT('',(-14.559884782075,0.100000000000152,-5.5));
#28771=CARTESIAN_POINT('Origin',(0.,0.,-5.5));
#28772=CARTESIAN_POINT('',(-14.7598894352984,0.100000000000155,-5.42720595314676));
#28773=CARTESIAN_POINT('Origin',(0.,0.,-5.42720595314676));
#28774=CARTESIAN_POINT('',(-0.0999999999999999,14.559884782075,-5.5));
#28775=CARTESIAN_POINT('',(-0.0999999999999999,14.559884782075,-5.5));
#28776=CARTESIAN_POINT('',(-10.2246825845813,10.3661039408188,-5.5));
#28777=CARTESIAN_POINT('Origin',(0.,0.,-5.5));
#28778=CARTESIAN_POINT('',(-10.3661072311444,10.507528587382,-5.42720595314676));
#28779=CARTESIAN_POINT('Origin',(0.,0.,-5.42720595314676));
#28780=CARTESIAN_POINT('',(0.0999999999999999,14.559884782075,-5.5));
#28781=CARTESIAN_POINT('',(10.2246825845814,10.3661039408187,-5.5));
#28782=CARTESIAN_POINT('Origin',(0.,0.,-5.5));
#28783=CARTESIAN_POINT('',(0.0999999999999999,14.7598894352984,-5.42720595314676));
#28784=CARTESIAN_POINT('',(10.2246825845814,10.3661039408187,-5.5));
#28785=CARTESIAN_POINT('Origin',(0.,0.,-5.5));
#28786=CARTESIAN_POINT('',(10.3079086644596,-10.1664873082224,-5.27388646312339));
#28787=CARTESIAN_POINT('',(10.3079086644596,-10.1664873082224,-5.27388646312339));
#28788=CARTESIAN_POINT('',(14.477584232982,-0.10000000000005,-5.27388646312339));
#28789=CARTESIAN_POINT('Origin',(0.,0.,-5.27388646312339));
#28790=CARTESIAN_POINT('',(14.559884782075,-0.100000000000051,-5.5));
#28791=CARTESIAN_POINT('Origin',(0.,0.,-5.5));
#28792=CARTESIAN_POINT('',(10.3079086644597,10.1664873082223,-5.27388646312339));
#28793=CARTESIAN_POINT('',(14.477584232982,0.0999999999999493,-5.27388646312339));
#28794=CARTESIAN_POINT('Origin',(0.,0.,-5.27388646312339));
#28795=CARTESIAN_POINT('',(10.3661039408187,10.2246825845814,-5.5));
#28796=CARTESIAN_POINT('',(14.477584232982,0.0999999999999493,-5.27388646312339));
#28797=CARTESIAN_POINT('Origin',(0.,0.,-5.5));
#28798=CARTESIAN_POINT('',(0.0999999999999999,-14.477584232982,-5.27388646312339));
#28799=CARTESIAN_POINT('',(0.0999999999999999,-14.477584232982,-5.27388646312339));
#28800=CARTESIAN_POINT('',(10.1664873082223,-10.3079086644597,-5.27388646312339));
#28801=CARTESIAN_POINT('Origin',(0.,0.,-5.27388646312339));
#28802=CARTESIAN_POINT('',(10.2246825845814,-10.3661039408188,-5.5));
#28803=CARTESIAN_POINT('Origin',(0.,0.,-5.5));
#28804=CARTESIAN_POINT('',(-10.1664873082224,-10.3079086644595,-5.27388646312339));
#28805=CARTESIAN_POINT('',(-10.1664873082224,-10.3079086644595,-5.27388646312339));
#28806=CARTESIAN_POINT('',(-0.0999999999999999,-14.477584232982,-5.27388646312339));
#28807=CARTESIAN_POINT('Origin',(0.,0.,-5.27388646312339));
#28808=CARTESIAN_POINT('',(-0.0999999999999999,-14.559884782075,-5.5));
#28809=CARTESIAN_POINT('Origin',(0.,0.,-5.5));
#28810=CARTESIAN_POINT('',(-14.477584232982,-0.0999999999998482,-5.27388646312339));
#28811=CARTESIAN_POINT('',(-14.477584232982,-0.0999999999998482,-5.27388646312339));
#28812=CARTESIAN_POINT('',(-10.3079086644597,-10.1664873082222,-5.27388646312339));
#28813=CARTESIAN_POINT('Origin',(0.,0.,-5.27388646312339));
#28814=CARTESIAN_POINT('',(-10.3661039408188,-10.2246825845813,-5.5));
#28815=CARTESIAN_POINT('Origin',(0.,0.,-5.5));
#28816=CARTESIAN_POINT('',(-10.3079086644595,10.1664873082225,-5.27388646312339));
#28817=CARTESIAN_POINT('',(-10.3079086644595,10.1664873082225,-5.27388646312339));
#28818=CARTESIAN_POINT('',(-14.477584232982,0.100000000000151,-5.27388646312339));
#28819=CARTESIAN_POINT('Origin',(0.,0.,-5.27388646312339));
#28820=CARTESIAN_POINT('',(-14.559884782075,0.100000000000152,-5.5));
#28821=CARTESIAN_POINT('Origin',(0.,0.,-5.5));
#28822=CARTESIAN_POINT('',(-0.0999999999999999,14.477584232982,-5.27388646312339));
#28823=CARTESIAN_POINT('',(-0.0999999999999999,14.477584232982,-5.27388646312339));
#28824=CARTESIAN_POINT('',(-10.1664873082222,10.3079086644598,-5.27388646312339));
#28825=CARTESIAN_POINT('Origin',(0.,0.,-5.27388646312339));
#28826=CARTESIAN_POINT('',(-10.2246825845813,10.3661039408188,-5.5));
#28827=CARTESIAN_POINT('Origin',(0.,0.,-5.5));
#28828=CARTESIAN_POINT('',(0.0999999999999999,14.477584232982,-5.27388646312339));
#28829=CARTESIAN_POINT('',(10.1664873082223,10.3079086644596,-5.27388646312339));
#28830=CARTESIAN_POINT('Origin',(0.,0.,-5.27388646312339));
#28831=CARTESIAN_POINT('',(0.0999999999999999,14.559884782075,-5.5));
#28832=CARTESIAN_POINT('',(10.1664873082223,10.3079086644596,-5.27388646312339));
#28833=CARTESIAN_POINT('Origin',(0.,0.,-5.27388646312339));
#28834=CARTESIAN_POINT('',(10.6195538920522,-10.478132535815,-4.64446921070048));
#28835=CARTESIAN_POINT('',(14.477584232982,-0.10000000000005,-5.27388646312339));
#28836=CARTESIAN_POINT('Origin',(0.,0.,-5.27388646312339));
#28837=CARTESIAN_POINT('',(10.3079086644597,10.1664873082223,-5.27388646312339));
#28838=CARTESIAN_POINT('',(14.9183171404923,0.0999999999999478,-4.64446921070048));
#28839=CARTESIAN_POINT('Origin',(0.,0.,-5.27388646312339));
#28840=CARTESIAN_POINT('',(0.0999999999999999,-14.9183171404923,-4.64446921070048));
#28841=CARTESIAN_POINT('',(10.1664873082223,-10.3079086644597,-5.27388646312339));
#28842=CARTESIAN_POINT('Origin',(0.,0.,-5.27388646312339));
#28843=CARTESIAN_POINT('',(-10.4781325358151,-10.6195538920522,-4.64446921070048));
#28844=CARTESIAN_POINT('',(-0.0999999999999999,-14.477584232982,-5.27388646312339));
#28845=CARTESIAN_POINT('Origin',(0.,0.,-5.27388646312339));
#28846=CARTESIAN_POINT('',(-14.9183171404923,-0.0999999999998437,-4.64446921070048));
#28847=CARTESIAN_POINT('',(-10.3079086644597,-10.1664873082222,-5.27388646312339));
#28848=CARTESIAN_POINT('Origin',(0.,0.,-5.27388646312339));
#28849=CARTESIAN_POINT('',(-10.6195538920522,10.4781325358151,-4.64446921070048));
#28850=CARTESIAN_POINT('',(-14.477584232982,0.100000000000151,-5.27388646312339));
#28851=CARTESIAN_POINT('Origin',(0.,0.,-5.27388646312339));
#28852=CARTESIAN_POINT('',(-0.0999999999999999,14.9183171404923,-4.64446921070048));
#28853=CARTESIAN_POINT('',(-10.1664873082222,10.3079086644598,-5.27388646312339));
#28854=CARTESIAN_POINT('Origin',(0.,0.,-5.27388646312339));
#28855=CARTESIAN_POINT('',(0.0999999999999999,14.477584232982,-5.27388646312339));
#28856=CARTESIAN_POINT('',(10.478132535815,10.6195538920523,-4.64446921070048));
#28857=CARTESIAN_POINT('Origin',(0.,8.781875,-5.5));
#28858=CARTESIAN_POINT('Origin',(0.,9.6875,-4.95));
#28859=CARTESIAN_POINT('Origin',(0.1,15.6,-5.5));
#28860=CARTESIAN_POINT('',(0.1,15.6,-4.64446921070048));
#28861=CARTESIAN_POINT('Origin',(-0.1,15.6,-5.5));
#28862=CARTESIAN_POINT('',(-0.1,15.6,-4.64446921070048));
#28863=CARTESIAN_POINT('Origin',(0.,0.,-4.64446921070048));
#28864=CARTESIAN_POINT('Origin',(11.1015764646288,10.9601551083915,-5.5));
#28865=CARTESIAN_POINT('',(11.1015764646288,10.9601551083915,-4.64446921070048));
#28866=CARTESIAN_POINT('Origin',(10.9601551083915,11.1015764646288,-5.5));
#28867=CARTESIAN_POINT('',(10.9601551083915,11.1015764646288,-4.64446921070048));
#28868=CARTESIAN_POINT('Origin',(0.,0.,-4.64446921070048));
#28869=CARTESIAN_POINT('Origin',(-10.9601551083914,11.1015764646289,-5.5));
#28870=CARTESIAN_POINT('',(-10.9601551083914,11.1015764646289,-4.64446921070048));
#28871=CARTESIAN_POINT('Origin',(-11.1015764646287,10.9601551083916,-5.5));
#28872=CARTESIAN_POINT('',(-11.1015764646287,10.9601551083916,-4.64446921070048));
#28873=CARTESIAN_POINT('Origin',(0.,0.,-4.64446921070048));
#28874=CARTESIAN_POINT('Origin',(-15.6,0.100000000000163,-5.5));
#28875=CARTESIAN_POINT('',(-15.6,0.100000000000163,-4.64446921070048));
#28876=CARTESIAN_POINT('Origin',(-15.6,-0.0999999999998366,-5.5));
#28877=CARTESIAN_POINT('',(-15.6,-0.0999999999998366,-4.64446921070048));
#28878=CARTESIAN_POINT('Origin',(0.,0.,-4.64446921070048));
#28879=CARTESIAN_POINT('Origin',(-11.1015764646289,-10.9601551083914,-5.5));
#28880=CARTESIAN_POINT('',(-11.1015764646289,-10.9601551083914,-4.64446921070048));
#28881=CARTESIAN_POINT('Origin',(-10.9601551083916,-11.1015764646287,-5.5));
#28882=CARTESIAN_POINT('',(-10.9601551083916,-11.1015764646287,-4.64446921070048));
#28883=CARTESIAN_POINT('Origin',(0.,0.,-4.64446921070048));
#28884=CARTESIAN_POINT('Origin',(-0.1,-15.6,-5.5));
#28885=CARTESIAN_POINT('',(-0.1,-15.6,-4.64446921070048));
#28886=CARTESIAN_POINT('Origin',(0.1,-15.6,-5.5));
#28887=CARTESIAN_POINT('',(0.1,-15.6,-4.64446921070048));
#28888=CARTESIAN_POINT('Origin',(0.,0.,-4.64446921070048));
#28889=CARTESIAN_POINT('Origin',(10.9601551083914,-11.1015764646289,-5.5));
#28890=CARTESIAN_POINT('',(10.9601551083914,-11.1015764646289,-4.64446921070048));
#28891=CARTESIAN_POINT('Origin',(11.1015764646287,-10.9601551083915,-5.5));
#28892=CARTESIAN_POINT('',(11.1015764646287,-10.9601551083915,-4.64446921070048));
#28893=CARTESIAN_POINT('Origin',(0.,0.,-4.64446921070048));
#28894=CARTESIAN_POINT('Origin',(15.6,-0.100000000000054,-5.5));
#28895=CARTESIAN_POINT('',(15.6,-0.100000000000054,-4.64446921070048));
#28896=CARTESIAN_POINT('Origin',(15.6,0.0999999999999455,-5.5));
#28897=CARTESIAN_POINT('',(15.6,0.0999999999999455,-4.64446921070048));
#28898=CARTESIAN_POINT('Origin',(0.,0.,-4.64446921070048));
#28899=CARTESIAN_POINT('Origin',(0.,12.03125,4.29391783951041E-16));
#28900=CARTESIAN_POINT('',(3.828125,12.03125,1.94986732551743E-16));
#28901=CARTESIAN_POINT('',(-3.828125,12.03125,1.94986732551743E-16));
#28902=CARTESIAN_POINT('Origin',(0.,12.03125,4.29391783951041E-16));
#28903=CARTESIAN_POINT('Origin',(0.,0.,4.29391783951041E-16));
#28904=CARTESIAN_POINT('',(-8.4375,1.03329573678058E-15,1.31890179813549));
#28905=CARTESIAN_POINT('Origin',(0.,0.,1.31890179813549));
#28906=CARTESIAN_POINT('',(-8.4375,-1.03329573678058E-15,-1.31890179813548));
#28907=CARTESIAN_POINT('Origin',(-12.03125,-1.47340318022416E-15,4.29391783951041E-16));
#28908=CARTESIAN_POINT('Origin',(0.,0.,-1.31890179813548));
#28909=CARTESIAN_POINT('Origin',(0.,0.,-4.99331957165859));
#28910=CARTESIAN_POINT('',(-5.44,-6.6620785873616E-16,-5.5));
#28911=CARTESIAN_POINT('Origin',(0.,0.,-5.5));
#28912=CARTESIAN_POINT('',(-5.10805041359455,-6.25555758889188E-16,-5.06034771053142));
#28913=CARTESIAN_POINT('Origin',(-5.65395079699728,-6.92409274607934E-16,
-4.99331957165859));
#28914=CARTESIAN_POINT('',(5.10805041359455,6.25555758889188E-16,-5.06034771053142));
#28915=CARTESIAN_POINT('Origin',(0.,0.,-5.06034771053142));
#28916=CARTESIAN_POINT('Origin',(0.,0.,-5.06034771053142));
#28917=CARTESIAN_POINT('Origin',(0.,0.,-4.18034771053142));
#28918=CARTESIAN_POINT('',(-5.,6.12323399573677E-16,-4.18034771053142));
#28919=CARTESIAN_POINT('',(5.,-6.12323399573677E-16,-4.18034771053142));
#28920=CARTESIAN_POINT('Origin',(0.,0.,-4.18034771053142));
#28921=CARTESIAN_POINT('',(5.,-6.12323399573677E-16,-4.18034771053142));
#28922=CARTESIAN_POINT('Origin',(0.,0.,-4.18034771053142));
#28923=CARTESIAN_POINT('Origin',(0.,0.,5.5));
#28924=CARTESIAN_POINT('',(-5.,-6.12323399573677E-16,4.18034771053142));
#28925=CARTESIAN_POINT('',(-5.,-6.12323399573677E-16,5.5));
#28926=CARTESIAN_POINT('Origin',(0.,0.,4.18034771053142));
#28927=CARTESIAN_POINT('Origin',(0.,0.,5.06034771053142));
#28928=CARTESIAN_POINT('',(-5.10805041359455,-6.25555758889188E-16,5.06034771053142));
#28929=CARTESIAN_POINT('',(-5.10805041359455,-6.25555758889188E-16,5.06034771053142));
#28930=CARTESIAN_POINT('Origin',(0.,0.,5.06034771053142));
#28931=CARTESIAN_POINT('Origin',(0.,0.,4.99331957165859));
#28932=CARTESIAN_POINT('',(-5.44,-6.6620785873616E-16,5.5));
#28933=CARTESIAN_POINT('Origin',(-5.65395079699728,-6.92409274607934E-16,
4.99331957165859));
#28934=CARTESIAN_POINT('Origin',(0.,0.,5.5));
#28935=CARTESIAN_POINT('Origin',(0.,0.,5.06034771053142));
#28936=CARTESIAN_POINT('',(-8.21796310590599,-1.00641022131588E-15,5.5));
#28937=CARTESIAN_POINT('Origin',(0.,0.,5.5));
#28938=CARTESIAN_POINT('',(-8.4375,-1.03329573678058E-15,5.06034771053142));
#28939=CARTESIAN_POINT('Origin',(-7.8875,-9.65940162827475E-16,5.06034771053142));
#28940=CARTESIAN_POINT('Origin',(0.,0.,5.06034771053142));
#28941=CARTESIAN_POINT('Origin',(0.,0.,-5.06034771053142));
#28942=CARTESIAN_POINT('',(-8.4375,-1.03329573678058E-15,-5.06034771053142));
#28943=CARTESIAN_POINT('Origin',(0.,0.,-5.06034771053142));
#28944=CARTESIAN_POINT('',(-8.21796310590599,-1.00641022131588E-15,-5.5));
#28945=CARTESIAN_POINT('Origin',(-7.8875,-9.65940162827475E-16,-5.06034771053142));
#28946=CARTESIAN_POINT('Origin',(0.,0.,-5.5));
#28947=CARTESIAN_POINT('Origin',(0.,0.,5.5));
#28948=CARTESIAN_POINT('',(-8.4375,-1.03329573678058E-15,5.5));
#28949=CARTESIAN_POINT('Origin',(0.,0.,5.5));
#28950=CARTESIAN_POINT('',(-8.4375,-1.03329573678058E-15,5.5));
#28951=CARTESIAN_POINT('Origin',(0.,8.21796310590599,5.5));
#28952=CARTESIAN_POINT('Origin',(0.,8.21796310590599,-5.5));
#28953=CARTESIAN_POINT('Origin',(0.,0.,4.29391783951041E-16));
#28954=CARTESIAN_POINT('',(-15.625,-1.91351062366774E-15,-1.31890179813548));
#28955=CARTESIAN_POINT('Origin',(0.,0.,-1.31890179813548));
#28956=CARTESIAN_POINT('',(-15.625,-1.91351062366774E-15,1.31890179813549));
#28957=CARTESIAN_POINT('Origin',(-12.03125,-1.47340318022416E-15,4.29391783951041E-16));
#28958=CARTESIAN_POINT('Origin',(0.,0.,1.31890179813549));
#28959=CARTESIAN_POINT('Origin',(0.,0.,5.5));
#28960=CARTESIAN_POINT('',(-17.5,-2.14313189850787E-15,4.92706821010937));
#28961=CARTESIAN_POINT('Origin',(0.,0.,4.92706821010937));
#28962=CARTESIAN_POINT('',(-17.5,-2.14313189850787E-15,-4.92706821010937));
#28963=CARTESIAN_POINT('',(-17.5,-2.14313189850787E-15,5.5));
#28964=CARTESIAN_POINT('Origin',(0.,0.,-4.92706821010937));
#28965=CARTESIAN_POINT('Origin',(0.,0.,-4.92706821010937));
#28966=CARTESIAN_POINT('',(-17.0170281388728,-2.08398490412711E-15,-5.4729685935121));
#28967=CARTESIAN_POINT('Origin',(-16.95,-2.07577632455476E-15,-4.92706821010937));
#28968=CARTESIAN_POINT('Origin',(0.,0.,-5.4729685935121));
#28969=CARTESIAN_POINT('Origin',(0.,0.,-5.5));
#28970=CARTESIAN_POINT('',(-16.796875,-2.05702392044282E-15,-5.5));
#28971=CARTESIAN_POINT('',(-16.796875,-2.05702392044282E-15,-5.5));
#28972=CARTESIAN_POINT('Origin',(0.,0.,-5.5));
#28973=CARTESIAN_POINT('Origin',(0.,0.,5.4729685935121));
#28974=CARTESIAN_POINT('',(-17.0170281388728,2.11355840131749E-15,5.4729685935121));
#28975=CARTESIAN_POINT('',(17.0170281388728,-2.08398490412711E-15,5.4729685935121));
#28976=CARTESIAN_POINT('Origin',(0.,0.,5.4729685935121));
#28977=CARTESIAN_POINT('',(16.796875,-2.05702392044282E-15,5.5));
#28978=CARTESIAN_POINT('',(17.0170281388728,-2.08398490412711E-15,5.4729685935121));
#28979=CARTESIAN_POINT('Origin',(0.,0.,5.5));
#28980=CARTESIAN_POINT('Origin',(0.,0.,5.4729685935121));
#28981=CARTESIAN_POINT('Origin',(0.,0.,4.92706821010937));
#28982=CARTESIAN_POINT('Origin',(-16.95,-2.07577632455476E-15,4.92706821010937));
#28983=CARTESIAN_POINT('Origin',(0.,0.,5.5));
#28984=CARTESIAN_POINT('',(-15.625,-1.91351062366774E-15,-5.5));
#28985=CARTESIAN_POINT('Origin',(0.,0.,-5.5));
#28986=CARTESIAN_POINT('',(-15.625,-1.91351062366774E-15,5.5));
#28987=CARTESIAN_POINT('Origin',(0.,0.,5.5));
#28988=CARTESIAN_POINT('',(-15.625,-1.91351062366774E-15,5.5));
#28989=CARTESIAN_POINT('',(-15.625,-1.91351062366774E-15,5.5));
#28990=CARTESIAN_POINT('Origin',(0.,0.,5.5));
#28991=CARTESIAN_POINT('Origin',(0.,16.796875,5.5));
#28992=CARTESIAN_POINT('Origin',(0.,16.796875,-5.5));
#28993=CARTESIAN_POINT('Origin',(8.50737846115067,8.50737846115064,4.29391783951041E-16));
#28994=CARTESIAN_POINT('',(11.2142716078804,5.80048531442088,1.94986732551743E-16));
#28995=CARTESIAN_POINT('',(5.80048531442092,11.2142716078804,1.94986732551743E-16));
#28996=CARTESIAN_POINT('Origin',(8.50737846115067,8.50737846115064,4.29391783951041E-16));
#28997=CARTESIAN_POINT('Origin',(12.03125,-4.20068848579565E-14,4.29391783951041E-16));
#28998=CARTESIAN_POINT('',(12.03125,-3.82812500000004,1.94986732551743E-16));
#28999=CARTESIAN_POINT('',(12.03125,3.82812499999996,1.94986732551743E-16));
#29000=CARTESIAN_POINT('Origin',(12.03125,-4.20068848579565E-14,4.29391783951041E-16));
#29001=CARTESIAN_POINT('Origin',(8.5073784611506,-8.5073784611507,4.29391783951041E-16));
#29002=CARTESIAN_POINT('',(5.80048531442084,-11.2142716078804,1.94986732551743E-16));
#29003=CARTESIAN_POINT('',(11.2142716078804,-5.80048531442096,1.94986732551743E-16));
#29004=CARTESIAN_POINT('Origin',(8.5073784611506,-8.5073784611507,4.29391783951041E-16));
#29005=CARTESIAN_POINT('Origin',(0.,-12.03125,4.29391783951041E-16));
#29006=CARTESIAN_POINT('',(-3.828125,-12.03125,1.94986732551743E-16));
#29007=CARTESIAN_POINT('',(3.828125,-12.03125,1.94986732551743E-16));
#29008=CARTESIAN_POINT('Origin',(0.,-12.03125,4.29391783951041E-16));
#29009=CARTESIAN_POINT('Origin',(-8.50737846115072,-8.50737846115057,4.29391783951041E-16));
#29010=CARTESIAN_POINT('',(-11.2142716078805,-5.8004853144208,1.94986732551743E-16));
#29011=CARTESIAN_POINT('',(-5.80048531442099,-11.2142716078804,1.94986732551743E-16));
#29012=CARTESIAN_POINT('Origin',(-8.50737846115072,-8.50737846115057,4.29391783951041E-16));
#29013=CARTESIAN_POINT('Origin',(-12.03125,1.26020654573869E-13,4.29391783951041E-16));
#29014=CARTESIAN_POINT('',(-12.03125,3.82812500000013,1.94986732551743E-16));
#29015=CARTESIAN_POINT('',(-12.03125,-3.82812499999988,1.94986732551743E-16));
#29016=CARTESIAN_POINT('Origin',(-12.03125,1.26020654573869E-13,4.29391783951041E-16));
#29017=CARTESIAN_POINT('Origin',(-8.50737846115055,8.50737846115075,4.29391783951041E-16));
#29018=CARTESIAN_POINT('',(-5.80048531442076,11.2142716078805,1.94986732551743E-16));
#29019=CARTESIAN_POINT('',(-11.2142716078803,5.80048531442103,1.94986732551743E-16));
#29020=CARTESIAN_POINT('Origin',(-8.50737846115055,8.50737846115075,4.29391783951041E-16));
#29021=CARTESIAN_POINT('Origin',(0.,0.,4.29391783951041E-16));
#29022=CARTESIAN_POINT('',(14.46011695371,1.78923010734816E-15,2.95890965336904));
#29023=CARTESIAN_POINT('',(-14.46011695371,-1.77085359426573E-15,2.95890965336904));
#29024=CARTESIAN_POINT('Origin',(0.,0.,2.95890965336904));
#29025=CARTESIAN_POINT('Origin',(0.,0.,2.95890965336904));
#29026=CARTESIAN_POINT('',(-12.9162151497931,-1.58178015402927E-15,3.72442984888649));
#29027=CARTESIAN_POINT('Origin',(-12.03125,-1.47340318022416E-15,4.29391783951041E-16));
#29028=CARTESIAN_POINT('',(12.9162151497931,1.58178015402927E-15,3.72442984888649));
#29029=CARTESIAN_POINT('Origin',(0.,0.,3.72442984888649));
#29030=CARTESIAN_POINT('Origin',(0.,0.,3.72442984888649));
#29031=CARTESIAN_POINT('Origin',(0.,0.,0.));
#29032=CARTESIAN_POINT('',(8.671875,-1.0619983961356E-15,5.39));
#29033=CARTESIAN_POINT('Origin',(0.,0.,5.39));
#29034=CARTESIAN_POINT('',(8.671875,-1.0619983961356E-15,4.95));
#29035=CARTESIAN_POINT('',(8.671875,-1.0619983961356E-15,0.));
#29036=CARTESIAN_POINT('Origin',(0.,0.,4.95));
#29037=CARTESIAN_POINT('Origin',(0.,0.,5.39));
#29038=CARTESIAN_POINT('',(8.781875,-1.07546951092622E-15,5.5));
#29039=CARTESIAN_POINT('Origin',(0.,0.,5.5));
#29040=CARTESIAN_POINT('Origin',(8.781875,-1.07546951092622E-15,5.39));
#29041=CARTESIAN_POINT('Origin',(0.,0.,0.10725138426002));
#29042=CARTESIAN_POINT('',(13.0772848379569,-1.60150550183421E-15,4.30142548471451));
#29043=CARTESIAN_POINT('Origin',(0.,0.,4.30142548471451));
#29044=CARTESIAN_POINT('',(9.6875,-1.186376586674E-15,5.5));
#29045=CARTESIAN_POINT('Origin',(9.6875,-1.186376586674E-15,0.10725138426002));
#29046=CARTESIAN_POINT('Origin',(0.,0.,5.5));
#29047=CARTESIAN_POINT('Origin',(0.,0.,3.66302186693758));
#29048=CARTESIAN_POINT('',(13.867180376262,-1.69823980609882E-15,3.66302186693758));
#29049=CARTESIAN_POINT('Origin',(0.,0.,3.66302186693758));
#29050=CARTESIAN_POINT('',(13.867180376262,-1.69823980609882E-15,3.66302186693758));
#29051=CARTESIAN_POINT('Origin',(0.,0.,4.22788751277274));
#29052=CARTESIAN_POINT('',(-14.9183171404923,-0.0999999999998437,4.64446921070048));
#29053=CARTESIAN_POINT('',(-14.9183171404923,0.100000000000156,4.64446921070048));
#29054=CARTESIAN_POINT('Origin',(0.,0.,4.64446921070048));
#29055=CARTESIAN_POINT('',(-10.6195538920524,-10.4781325358149,4.64446921070048));
#29056=CARTESIAN_POINT('Origin',(0.,0.,4.64446921070048));
#29057=CARTESIAN_POINT('',(-10.4781325358151,-10.6195538920522,4.64446921070048));
#29058=CARTESIAN_POINT('Origin',(0.,0.,4.64446921070048));
#29059=CARTESIAN_POINT('',(-0.0999999999999999,-14.9183171404923,4.64446921070048));
#29060=CARTESIAN_POINT('Origin',(0.,0.,4.64446921070048));
#29061=CARTESIAN_POINT('',(0.0999999999999999,-14.9183171404923,4.64446921070048));
#29062=CARTESIAN_POINT('Origin',(0.,0.,4.64446921070048));
#29063=CARTESIAN_POINT('',(10.4781325358149,-10.6195538920523,4.64446921070048));
#29064=CARTESIAN_POINT('Origin',(0.,0.,4.64446921070048));
#29065=CARTESIAN_POINT('',(10.6195538920522,-10.478132535815,4.64446921070048));
#29066=CARTESIAN_POINT('Origin',(0.,0.,4.64446921070048));
#29067=CARTESIAN_POINT('',(14.9183171404923,-0.100000000000052,4.64446921070048));
#29068=CARTESIAN_POINT('Origin',(0.,0.,4.64446921070048));
#29069=CARTESIAN_POINT('',(14.9186522951742,-1.82700797808774E-15,4.64446921070048));
#29070=CARTESIAN_POINT('Origin',(0.,0.,4.64446921070048));
#29071=CARTESIAN_POINT('Origin',(14.3237119736335,-1.75414880204189E-15,
4.22788751277274));
#29072=CARTESIAN_POINT('',(14.9183171404923,0.0999999999999478,4.64446921070048));
#29073=CARTESIAN_POINT('Origin',(0.,0.,4.64446921070048));
#29074=CARTESIAN_POINT('',(10.6195538920523,10.478132535815,4.64446921070048));
#29075=CARTESIAN_POINT('Origin',(0.,0.,4.64446921070048));
#29076=CARTESIAN_POINT('',(10.478132535815,10.6195538920523,4.64446921070048));
#29077=CARTESIAN_POINT('Origin',(0.,0.,4.64446921070048));
#29078=CARTESIAN_POINT('',(0.0999999999999999,14.9183171404923,4.64446921070048));
#29079=CARTESIAN_POINT('Origin',(0.,0.,4.64446921070048));
#29080=CARTESIAN_POINT('',(-0.0999999999999999,14.9183171404923,4.64446921070048));
#29081=CARTESIAN_POINT('Origin',(0.,0.,4.64446921070048));
#29082=CARTESIAN_POINT('',(-10.4781325358149,10.6195538920524,4.64446921070048));
#29083=CARTESIAN_POINT('Origin',(0.,0.,4.64446921070048));
#29084=CARTESIAN_POINT('',(-10.6195538920522,10.4781325358151,4.64446921070048));
#29085=CARTESIAN_POINT('Origin',(0.,0.,4.64446921070048));
#29086=CARTESIAN_POINT('Origin',(0.,0.,4.64446921070048));
#29087=CARTESIAN_POINT('Origin',(0.,0.,0.10725138426002));
#29088=CARTESIAN_POINT('',(9.6875,-1.186376586674E-15,4.95));
#29089=CARTESIAN_POINT('Origin',(0.,0.,4.95));
#29090=CARTESIAN_POINT('',(12.7315647249454,-1.55916699885417E-15,3.87366667012467));
#29091=CARTESIAN_POINT('Origin',(9.6875,-1.186376586674E-15,0.10725138426002));
#29092=CARTESIAN_POINT('Origin',(0.,0.,3.87366667012467));
#29093=CARTESIAN_POINT('Origin',(0.,0.,3.87366667012467));
#29094=CARTESIAN_POINT('',(12.7315647249454,-1.55916699885417E-15,3.87366667012467));
#29095=CARTESIAN_POINT('Origin',(0.,0.,4.22788751277274));
#29096=CARTESIAN_POINT('',(15.5300994798678,-1.901888661846E-15,4.64446921070048));
#29097=CARTESIAN_POINT('Origin',(14.3237119736335,-1.75414880204189E-15,
4.22788751277274));
#29098=CARTESIAN_POINT('',(15.5297775210912,-0.100000000000054,4.64446921070048));
#29099=CARTESIAN_POINT('Origin',(0.,0.,4.64446921070048));
#29100=CARTESIAN_POINT('',(14.7598894352984,-0.100000000000051,5.42720595314676));
#29101=CARTESIAN_POINT('Origin',(14.3233830013084,-0.100000000000069,4.22787124927498));
#29102=CARTESIAN_POINT('',(10.5075285873818,-10.3661072311446,5.42720595314676));
#29103=CARTESIAN_POINT('Origin',(0.,0.,5.42720595314676));
#29104=CARTESIAN_POINT('',(11.0519216736006,-10.9105003173634,4.64446921070048));
#29105=CARTESIAN_POINT('Origin',(10.1988719218254,-10.0574505655883,4.22787124085885));
#29106=CARTESIAN_POINT('',(10.9105003173633,-11.0519216736007,4.64446921070048));
#29107=CARTESIAN_POINT('Origin',(0.,0.,4.64446921070048));
#29108=CARTESIAN_POINT('',(10.3661072311445,-10.5075285873819,5.42720595314676));
#29109=CARTESIAN_POINT('Origin',(10.0574505716385,-10.198871927876,4.22787124927498));
#29110=CARTESIAN_POINT('',(0.0999999999999999,-14.7598894352984,5.42720595314676));
#29111=CARTESIAN_POINT('Origin',(0.,0.,5.42720595314676));
#29112=CARTESIAN_POINT('',(0.1,-15.5297775210912,4.64446921070048));
#29113=CARTESIAN_POINT('Origin',(0.099999999999988,-14.3233829927518,4.22787124085886));
#29114=CARTESIAN_POINT('',(-0.1,-15.5297775210912,4.64446921070048));
#29115=CARTESIAN_POINT('Origin',(0.,0.,4.64446921070048));
#29116=CARTESIAN_POINT('',(-0.0999999999999999,-14.7598894352984,5.42720595314676));
#29117=CARTESIAN_POINT('Origin',(-0.100000000000002,-14.3233830013084,4.22787124927497));
#29118=CARTESIAN_POINT('',(-10.3661072311446,-10.5075285873818,5.42720595314676));
#29119=CARTESIAN_POINT('Origin',(0.,0.,5.42720595314676));
#29120=CARTESIAN_POINT('',(-10.9105003173634,-11.0519216736006,4.64446921070048));
#29121=CARTESIAN_POINT('Origin',(-10.0574505655883,-10.1988719218254,4.22787124085886));
#29122=CARTESIAN_POINT('',(-11.0519216736007,-10.9105003173632,4.64446921070048));
#29123=CARTESIAN_POINT('Origin',(0.,0.,4.64446921070048));
#29124=CARTESIAN_POINT('',(-10.5075285873819,-10.3661072311445,5.42720595314676));
#29125=CARTESIAN_POINT('Origin',(-10.198871927876,-10.0574505716385,4.22787124927499));
#29126=CARTESIAN_POINT('',(-14.7598894352984,-0.0999999999998453,5.42720595314676));
#29127=CARTESIAN_POINT('Origin',(0.,0.,5.42720595314676));
#29128=CARTESIAN_POINT('',(-15.5297775210912,-0.0999999999998373,4.64446921070048));
#29129=CARTESIAN_POINT('Origin',(-14.3233829927518,-0.0999999999998497,
4.22787124085885));
#29130=CARTESIAN_POINT('',(-15.5297775210912,0.100000000000163,4.64446921070048));
#29131=CARTESIAN_POINT('Origin',(0.,0.,4.64446921070048));
#29132=CARTESIAN_POINT('',(-14.7598894352984,0.100000000000155,5.42720595314676));
#29133=CARTESIAN_POINT('Origin',(-14.3233830013084,0.10000000000015,4.227871249275));
#29134=CARTESIAN_POINT('',(-10.5075285873817,10.3661072311447,5.42720595314676));
#29135=CARTESIAN_POINT('Origin',(0.,0.,5.42720595314676));
#29136=CARTESIAN_POINT('',(-11.0519216736005,10.9105003173635,4.64446921070048));
#29137=CARTESIAN_POINT('Origin',(-10.1988719218254,10.0574505655883,4.22787124085886));
#29138=CARTESIAN_POINT('',(-10.9105003173632,11.0519216736008,4.64446921070048));
#29139=CARTESIAN_POINT('Origin',(0.,0.,4.64446921070048));
#29140=CARTESIAN_POINT('',(-10.3661072311444,10.507528587382,5.42720595314676));
#29141=CARTESIAN_POINT('Origin',(-10.0574505716385,10.1988719278761,4.22787124927498));
#29142=CARTESIAN_POINT('',(-0.0999999999999999,14.7598894352984,5.42720595314676));
#29143=CARTESIAN_POINT('Origin',(0.,0.,5.42720595314676));
#29144=CARTESIAN_POINT('',(-0.1,15.5297775210912,4.64446921070048));
#29145=CARTESIAN_POINT('Origin',(-0.100000000000018,14.3233829927518,4.22787124085886));
#29146=CARTESIAN_POINT('',(0.1,15.5297775210912,4.64446921070048));
#29147=CARTESIAN_POINT('Origin',(0.,0.,4.64446921070048));
#29148=CARTESIAN_POINT('',(0.0999999999999999,14.7598894352984,5.42720595314676));
#29149=CARTESIAN_POINT('Origin',(0.100000000000003,14.3233830013084,4.22787124927497));
#29150=CARTESIAN_POINT('',(10.3661072311446,10.5075285873818,5.42720595314676));
#29151=CARTESIAN_POINT('Origin',(0.,0.,5.42720595314676));
#29152=CARTESIAN_POINT('',(10.9105003173634,11.0519216736006,4.64446921070048));
#29153=CARTESIAN_POINT('Origin',(10.0574505655882,10.1988719218255,4.22787124085886));
#29154=CARTESIAN_POINT('',(11.0519216736007,10.9105003173633,4.64446921070048));
#29155=CARTESIAN_POINT('Origin',(0.,0.,4.64446921070048));
#29156=CARTESIAN_POINT('',(10.5075285873819,10.3661072311445,5.42720595314676));
#29157=CARTESIAN_POINT('Origin',(10.1988719278759,10.0574505716386,4.22787124927498));
#29158=CARTESIAN_POINT('',(14.7598894352984,0.0999999999999484,5.42720595314676));
#29159=CARTESIAN_POINT('Origin',(0.,0.,5.42720595314676));
#29160=CARTESIAN_POINT('',(15.5297775210912,0.0999999999999458,4.64446921070048));
#29161=CARTESIAN_POINT('Origin',(14.3233829927518,0.0999999999999847,4.22787124085886));
#29162=CARTESIAN_POINT('Origin',(0.,0.,4.64446921070048));
#29163=CARTESIAN_POINT('Origin',(0.,0.,5.42720595314676));
#29164=CARTESIAN_POINT('',(14.559884782075,-0.100000000000051,5.5));
#29165=CARTESIAN_POINT('',(14.7598894352984,-0.100000000000051,5.42720595314676));
#29166=CARTESIAN_POINT('',(10.3661039408187,-10.2246825845815,5.5));
#29167=CARTESIAN_POINT('Origin',(0.,0.,5.5));
#29168=CARTESIAN_POINT('',(10.3661039408187,-10.2246825845815,5.5));
#29169=CARTESIAN_POINT('Origin',(0.,0.,5.42720595314676));
#29170=CARTESIAN_POINT('',(10.3661039408187,10.2246825845814,5.5));
#29171=CARTESIAN_POINT('',(14.559884782075,0.099999999999949,5.5));
#29172=CARTESIAN_POINT('Origin',(0.,0.,5.5));
#29173=CARTESIAN_POINT('',(14.559884782075,0.099999999999949,5.5));
#29174=CARTESIAN_POINT('',(10.5075285873819,10.3661072311445,5.42720595314676));
#29175=CARTESIAN_POINT('Origin',(0.,0.,5.42720595314676));
#29176=CARTESIAN_POINT('',(10.2246825845814,-10.3661039408188,5.5));
#29177=CARTESIAN_POINT('',(10.3661072311445,-10.5075285873819,5.42720595314676));
#29178=CARTESIAN_POINT('',(0.0999999999999999,-14.559884782075,5.5));
#29179=CARTESIAN_POINT('Origin',(0.,0.,5.5));
#29180=CARTESIAN_POINT('',(0.0999999999999999,-14.559884782075,5.5));
#29181=CARTESIAN_POINT('Origin',(0.,0.,5.42720595314676));
#29182=CARTESIAN_POINT('',(-0.0999999999999999,-14.559884782075,5.5));
#29183=CARTESIAN_POINT('',(-0.0999999999999999,-14.7598894352984,5.42720595314676));
#29184=CARTESIAN_POINT('',(-10.2246825845815,-10.3661039408186,5.5));
#29185=CARTESIAN_POINT('Origin',(0.,0.,5.5));
#29186=CARTESIAN_POINT('',(-10.2246825845815,-10.3661039408186,5.5));
#29187=CARTESIAN_POINT('Origin',(0.,0.,5.42720595314676));
#29188=CARTESIAN_POINT('',(-10.3661039408188,-10.2246825845813,5.5));
#29189=CARTESIAN_POINT('',(-10.5075285873819,-10.3661072311445,5.42720595314676));
#29190=CARTESIAN_POINT('',(-14.559884782075,-0.0999999999998474,5.5));
#29191=CARTESIAN_POINT('Origin',(0.,0.,5.5));
#29192=CARTESIAN_POINT('',(-14.559884782075,-0.0999999999998474,5.5));
#29193=CARTESIAN_POINT('Origin',(0.,0.,5.42720595314676));
#29194=CARTESIAN_POINT('',(-14.559884782075,0.100000000000152,5.5));
#29195=CARTESIAN_POINT('',(-14.7598894352984,0.100000000000155,5.42720595314676));
#29196=CARTESIAN_POINT('',(-10.3661039408186,10.2246825845815,5.5));
#29197=CARTESIAN_POINT('Origin',(0.,0.,5.5));
#29198=CARTESIAN_POINT('',(-10.3661039408186,10.2246825845815,5.5));
#29199=CARTESIAN_POINT('Origin',(0.,0.,5.42720595314676));
#29200=CARTESIAN_POINT('',(-10.2246825845813,10.3661039408188,5.5));
#29201=CARTESIAN_POINT('',(-10.3661072311444,10.507528587382,5.42720595314676));
#29202=CARTESIAN_POINT('',(-0.0999999999999999,14.559884782075,5.5));
#29203=CARTESIAN_POINT('Origin',(0.,0.,5.5));
#29204=CARTESIAN_POINT('',(-0.0999999999999999,14.559884782075,5.5));
#29205=CARTESIAN_POINT('Origin',(0.,0.,5.42720595314676));
#29206=CARTESIAN_POINT('',(0.0999999999999999,14.559884782075,5.5));
#29207=CARTESIAN_POINT('',(10.2246825845814,10.3661039408187,5.5));
#29208=CARTESIAN_POINT('Origin',(0.,0.,5.5));
#29209=CARTESIAN_POINT('',(10.2246825845814,10.3661039408187,5.5));
#29210=CARTESIAN_POINT('',(0.0999999999999999,14.7598894352984,5.42720595314676));
#29211=CARTESIAN_POINT('Origin',(0.,0.,5.5));
#29212=CARTESIAN_POINT('',(14.477584232982,-0.10000000000005,5.27388646312339));
#29213=CARTESIAN_POINT('',(14.559884782075,-0.100000000000051,5.5));
#29214=CARTESIAN_POINT('',(10.3079086644596,-10.1664873082224,5.27388646312339));
#29215=CARTESIAN_POINT('Origin',(0.,0.,5.27388646312339));
#29216=CARTESIAN_POINT('',(10.3079086644596,-10.1664873082224,5.27388646312339));
#29217=CARTESIAN_POINT('Origin',(0.,0.,5.5));
#29218=CARTESIAN_POINT('',(10.3079086644597,10.1664873082223,5.27388646312339));
#29219=CARTESIAN_POINT('',(14.477584232982,0.0999999999999493,5.27388646312339));
#29220=CARTESIAN_POINT('Origin',(0.,0.,5.27388646312339));
#29221=CARTESIAN_POINT('',(14.477584232982,0.0999999999999493,5.27388646312339));
#29222=CARTESIAN_POINT('',(10.3661039408187,10.2246825845814,5.5));
#29223=CARTESIAN_POINT('Origin',(0.,0.,5.5));
#29224=CARTESIAN_POINT('',(10.1664873082223,-10.3079086644597,5.27388646312339));
#29225=CARTESIAN_POINT('',(10.2246825845814,-10.3661039408188,5.5));
#29226=CARTESIAN_POINT('',(0.0999999999999999,-14.477584232982,5.27388646312339));
#29227=CARTESIAN_POINT('Origin',(0.,0.,5.27388646312339));
#29228=CARTESIAN_POINT('',(0.0999999999999999,-14.477584232982,5.27388646312339));
#29229=CARTESIAN_POINT('Origin',(0.,0.,5.5));
#29230=CARTESIAN_POINT('',(-0.0999999999999999,-14.477584232982,5.27388646312339));
#29231=CARTESIAN_POINT('',(-0.0999999999999999,-14.559884782075,5.5));
#29232=CARTESIAN_POINT('',(-10.1664873082224,-10.3079086644595,5.27388646312339));
#29233=CARTESIAN_POINT('Origin',(0.,0.,5.27388646312339));
#29234=CARTESIAN_POINT('',(-10.1664873082224,-10.3079086644595,5.27388646312339));
#29235=CARTESIAN_POINT('Origin',(0.,0.,5.5));
#29236=CARTESIAN_POINT('',(-10.3079086644597,-10.1664873082222,5.27388646312339));
#29237=CARTESIAN_POINT('',(-10.3661039408188,-10.2246825845813,5.5));
#29238=CARTESIAN_POINT('',(-14.477584232982,-0.0999999999998482,5.27388646312339));
#29239=CARTESIAN_POINT('Origin',(0.,0.,5.27388646312339));
#29240=CARTESIAN_POINT('',(-14.477584232982,-0.0999999999998482,5.27388646312339));
#29241=CARTESIAN_POINT('Origin',(0.,0.,5.5));
#29242=CARTESIAN_POINT('',(-14.477584232982,0.100000000000151,5.27388646312339));
#29243=CARTESIAN_POINT('',(-14.559884782075,0.100000000000152,5.5));
#29244=CARTESIAN_POINT('',(-10.3079086644595,10.1664873082225,5.27388646312339));
#29245=CARTESIAN_POINT('Origin',(0.,0.,5.27388646312339));
#29246=CARTESIAN_POINT('',(-10.3079086644595,10.1664873082225,5.27388646312339));
#29247=CARTESIAN_POINT('Origin',(0.,0.,5.5));
#29248=CARTESIAN_POINT('',(-10.1664873082222,10.3079086644598,5.27388646312339));
#29249=CARTESIAN_POINT('',(-10.2246825845813,10.3661039408188,5.5));
#29250=CARTESIAN_POINT('',(-0.0999999999999999,14.477584232982,5.27388646312339));
#29251=CARTESIAN_POINT('Origin',(0.,0.,5.27388646312339));
#29252=CARTESIAN_POINT('',(-0.0999999999999999,14.477584232982,5.27388646312339));
#29253=CARTESIAN_POINT('Origin',(0.,0.,5.5));
#29254=CARTESIAN_POINT('',(0.0999999999999999,14.477584232982,5.27388646312339));
#29255=CARTESIAN_POINT('',(10.1664873082223,10.3079086644596,5.27388646312339));
#29256=CARTESIAN_POINT('Origin',(0.,0.,5.27388646312339));
#29257=CARTESIAN_POINT('',(10.1664873082223,10.3079086644596,5.27388646312339));
#29258=CARTESIAN_POINT('',(0.0999999999999999,14.559884782075,5.5));
#29259=CARTESIAN_POINT('Origin',(0.,0.,5.27388646312339));
#29260=CARTESIAN_POINT('',(14.477584232982,-0.10000000000005,5.27388646312339));
#29261=CARTESIAN_POINT('',(10.6195538920522,-10.478132535815,4.64446921070048));
#29262=CARTESIAN_POINT('Origin',(0.,0.,5.27388646312339));
#29263=CARTESIAN_POINT('',(14.9183171404923,0.0999999999999478,4.64446921070048));
#29264=CARTESIAN_POINT('',(10.3079086644597,10.1664873082223,5.27388646312339));
#29265=CARTESIAN_POINT('Origin',(0.,0.,5.27388646312339));
#29266=CARTESIAN_POINT('',(10.1664873082223,-10.3079086644597,5.27388646312339));
#29267=CARTESIAN_POINT('',(0.0999999999999999,-14.9183171404923,4.64446921070048));
#29268=CARTESIAN_POINT('Origin',(0.,0.,5.27388646312339));
#29269=CARTESIAN_POINT('',(-0.0999999999999999,-14.477584232982,5.27388646312339));
#29270=CARTESIAN_POINT('',(-10.4781325358151,-10.6195538920522,4.64446921070048));
#29271=CARTESIAN_POINT('Origin',(0.,0.,5.27388646312339));
#29272=CARTESIAN_POINT('',(-10.3079086644597,-10.1664873082222,5.27388646312339));
#29273=CARTESIAN_POINT('',(-14.9183171404923,-0.0999999999998437,4.64446921070048));
#29274=CARTESIAN_POINT('Origin',(0.,0.,5.27388646312339));
#29275=CARTESIAN_POINT('',(-14.477584232982,0.100000000000151,5.27388646312339));
#29276=CARTESIAN_POINT('',(-10.6195538920522,10.4781325358151,4.64446921070048));
#29277=CARTESIAN_POINT('Origin',(0.,0.,5.27388646312339));
#29278=CARTESIAN_POINT('',(-10.1664873082222,10.3079086644598,5.27388646312339));
#29279=CARTESIAN_POINT('',(-0.0999999999999999,14.9183171404923,4.64446921070048));
#29280=CARTESIAN_POINT('Origin',(0.,0.,5.27388646312339));
#29281=CARTESIAN_POINT('',(10.478132535815,10.6195538920523,4.64446921070048));
#29282=CARTESIAN_POINT('',(0.0999999999999999,14.477584232982,5.27388646312339));
#29283=CARTESIAN_POINT('Origin',(0.,8.781875,5.5));
#29284=CARTESIAN_POINT('Origin',(0.,9.6875,4.95));
#29285=CARTESIAN_POINT('Origin',(0.1,15.6,5.5));
#29286=CARTESIAN_POINT('',(0.1,15.6,4.64446921070048));
#29287=CARTESIAN_POINT('Origin',(-0.1,15.6,5.5));
#29288=CARTESIAN_POINT('',(-0.1,15.6,4.64446921070048));
#29289=CARTESIAN_POINT('Origin',(0.,0.,4.64446921070048));
#29290=CARTESIAN_POINT('Origin',(11.1015764646288,10.9601551083915,5.5));
#29291=CARTESIAN_POINT('',(11.1015764646288,10.9601551083915,4.64446921070048));
#29292=CARTESIAN_POINT('Origin',(10.9601551083915,11.1015764646288,5.5));
#29293=CARTESIAN_POINT('',(10.9601551083915,11.1015764646288,4.64446921070048));
#29294=CARTESIAN_POINT('Origin',(0.,0.,4.64446921070048));
#29295=CARTESIAN_POINT('Origin',(-10.9601551083914,11.1015764646289,5.5));
#29296=CARTESIAN_POINT('',(-10.9601551083914,11.1015764646289,4.64446921070048));
#29297=CARTESIAN_POINT('Origin',(-11.1015764646287,10.9601551083916,5.5));
#29298=CARTESIAN_POINT('',(-11.1015764646287,10.9601551083916,4.64446921070048));
#29299=CARTESIAN_POINT('Origin',(0.,0.,4.64446921070048));
#29300=CARTESIAN_POINT('Origin',(-15.6,0.100000000000163,5.5));
#29301=CARTESIAN_POINT('',(-15.6,0.100000000000163,4.64446921070048));
#29302=CARTESIAN_POINT('Origin',(-15.6,-0.0999999999998366,5.5));
#29303=CARTESIAN_POINT('',(-15.6,-0.0999999999998366,4.64446921070048));
#29304=CARTESIAN_POINT('Origin',(0.,0.,4.64446921070048));
#29305=CARTESIAN_POINT('Origin',(-11.1015764646289,-10.9601551083914,5.5));
#29306=CARTESIAN_POINT('',(-11.1015764646289,-10.9601551083914,4.64446921070048));
#29307=CARTESIAN_POINT('Origin',(-10.9601551083916,-11.1015764646287,5.5));
#29308=CARTESIAN_POINT('',(-10.9601551083916,-11.1015764646287,4.64446921070048));
#29309=CARTESIAN_POINT('Origin',(0.,0.,4.64446921070048));
#29310=CARTESIAN_POINT('Origin',(-0.1,-15.6,5.5));
#29311=CARTESIAN_POINT('',(-0.1,-15.6,4.64446921070048));
#29312=CARTESIAN_POINT('Origin',(0.1,-15.6,5.5));
#29313=CARTESIAN_POINT('',(0.1,-15.6,4.64446921070048));
#29314=CARTESIAN_POINT('Origin',(0.,0.,4.64446921070048));
#29315=CARTESIAN_POINT('Origin',(10.9601551083914,-11.1015764646289,5.5));
#29316=CARTESIAN_POINT('',(10.9601551083914,-11.1015764646289,4.64446921070048));
#29317=CARTESIAN_POINT('Origin',(11.1015764646287,-10.9601551083915,5.5));
#29318=CARTESIAN_POINT('',(11.1015764646287,-10.9601551083915,4.64446921070048));
#29319=CARTESIAN_POINT('Origin',(0.,0.,4.64446921070048));
#29320=CARTESIAN_POINT('Origin',(15.6,-0.100000000000054,5.5));
#29321=CARTESIAN_POINT('',(15.6,-0.100000000000054,4.64446921070048));
#29322=CARTESIAN_POINT('Origin',(15.6,0.0999999999999455,5.5));
#29323=CARTESIAN_POINT('',(15.6,0.0999999999999455,4.64446921070048));
#29324=CARTESIAN_POINT('Origin',(0.,0.,4.64446921070048));
#48347=UNCERTAINTY_MEASURE_WITH_UNIT(LENGTH_MEASURE(0.01),#48370,
'DISTANCE_ACCURACY_VALUE',
'Maximum model space distance between geometric entities at asserted c
onnectivities');
#48356=UNCERTAINTY_MEASURE_WITH_UNIT(LENGTH_MEASURE(0.01),#48370,
'DISTANCE_ACCURACY_VALUE',
'Maximum model space distance between geometric entities at asserted c
onnectivities');
#48360=(
GEOMETRIC_REPRESENTATION_CONTEXT(3)
GLOBAL_UNCERTAINTY_ASSIGNED_CONTEXT((#48347))
GLOBAL_UNIT_ASSIGNED_CONTEXT((#48370,#48372,#48373))
REPRESENTATION_CONTEXT('','3D')
);
#48369=(
GEOMETRIC_REPRESENTATION_CONTEXT(3)
GLOBAL_UNCERTAINTY_ASSIGNED_CONTEXT((#48356))
GLOBAL_UNIT_ASSIGNED_CONTEXT((#48370,#48372,#48373))
REPRESENTATION_CONTEXT('','3D')
);
#48370=(
LENGTH_UNIT()
NAMED_UNIT(*)
SI_UNIT(.MILLI.,.METRE.)
);
#48372=(
NAMED_UNIT(*)
PLANE_ANGLE_UNIT()
SI_UNIT($,.RADIAN.)
);
#48373=(
NAMED_UNIT(*)
SI_UNIT($,.STERADIAN.)
SOLID_ANGLE_UNIT()
);
#48377=SHAPE_DEFINITION_REPRESENTATION(#48389,#48415);
#48389=PRODUCT_DEFINITION_SHAPE('',$,#48428);
#48415=SHAPE_REPRESENTATION('',(#20727),#48360);
#48424=PRODUCT_DEFINITION_CONTEXT('part definition',#48462,'design');
#48428=PRODUCT_DEFINITION('6661K61_Steel Ball Bearing',
'6661K61_Steel Ball Bearing',#48440,#48424);
#48440=PRODUCT_DEFINITION_FORMATION('',$,#48467);
#48462=APPLICATION_CONTEXT(
'Core Data for Automotive Mechanical Design Process');
#48463=PRODUCT_CONTEXT('part definition',#48462,'mechanical');
#48467=PRODUCT('6661K61_Steel Ball Bearing',
'6661K61_Steel Ball Bearing',$,(#48463));
#48511=COLOUR_RGB('Grey',0.48,0.52,0.57);
#48512=FILL_AREA_STYLE_COLOUR('',#48511);
#48513=FILL_AREA_STYLE('',(#48512));
#48514=SURFACE_STYLE_FILL_AREA(#48513);
#48515=SURFACE_SIDE_STYLE('',(#48514));
#48516=SURFACE_STYLE_USAGE(.BOTH.,#48515);
#48517=PRESENTATION_STYLE_ASSIGNMENT((#48516));
ENDSEC;
END-ISO-10303-21;
